ISO-10303-21;
HEADER;
FILE_DESCRIPTION (('STEP AP214'),
    '1' );
FILE_NAME ('hex flange nut gradea_iso_ISO - 4161 - M5 - N.step',
    '2026-10-06T08:09:25',
    ( '' ),
    ( '' ),
    'SwSTEP 2.0',
    'SolidWorks 2021',
    '' );
FILE_SCHEMA (( 'AUTOMOTIVE_DESIGN' ));
ENDSEC;

DATA;
#72=FACE_OUTER_BOUND ( 'NONE', #12536, .T. ) ;
#77=CARTESIAN_POINT ( 'NONE',  ( -2.836893136758718903, -3.208949435745849676, -3.505054077164919235 ) ) ;
#85=( NAMED_UNIT ( * ) PLANE_ANGLE_UNIT ( ) SI_UNIT ( $, .RADIAN. ) );
#106=CARTESIAN_POINT ( 'NONE',  ( -2.725741868434905513, 3.045094352034741547, -3.220599429844064332 ) ) ;
#116=CARTESIAN_POINT ( 'NONE',  ( 2.712762565639641021, -3.052587955997488223, -3.430618716626634424 ) ) ;
#133=AXIS2_PLACEMENT_3D ( 'NONE', #13173, #11168, #18350 ) ;
#142=ORIENTED_EDGE ( 'NONE', *, *, #22317, .T. ) ;
#174=EDGE_CURVE ( 'NONE', #11003, #22641, #9065, .T. ) ;
#177=EDGE_LOOP ( 'NONE', ( #17810, #15690, #3320, #5048, #142 ) ) ;
#186=EDGE_CURVE ( 'NONE', #15772, #2089, #3930, .T. ) ;
#214=B_SPLINE_CURVE_WITH_KNOTS ( 'NONE', 3,
 ( #18119, #8839, #16105, #19776, #9183, #244, #12819, #19998 ),
 .UNSPECIFIED., .F., .F.,
 ( 4, 2, 2, 4 ),
 ( 0.005725059856848683376, 0.006314084072593680388, 0.006903108288338678268, 0.008081156719828673160 ),
 .UNSPECIFIED. ) ;
#237=DIRECTION ( 'NONE',  ( 1.333893503340774882E-15, 2.778352770573747380E-17, 1.000000000000000000 ) ) ;
#244=CARTESIAN_POINT ( 'NONE',  ( 3.999999999999940048, 1.563622288139227656, -0.2253451193527943042 ) ) ;
#293=CARTESIAN_POINT ( 'NONE',  ( -4.211140560182312420, 2.431303136016568889, -3.745885042887433958 ) ) ;
#361=B_SPLINE_CURVE_WITH_KNOTS ( 'NONE', 3,
 ( #6764, #4763, #1473, #6888, #3009, #3129, #13933, #11933 ),
 .UNSPECIFIED., .F., .F.,
 ( 4, 2, 2, 4 ),
 ( 0.000000000000000000, 0.002450665683189822298, 0.003675998524784733663, 0.004901331366379645463 ),
 .UNSPECIFIED. ) ;
#364=CARTESIAN_POINT ( 'NONE',  ( 1.999999999999974021, 3.464101615137785029, 3.469446951953614189E-15 ) ) ;
#368=EDGE_CURVE ( 'NONE', #2382, #9560, #3409, .T. ) ;
#385=CARTESIAN_POINT ( 'NONE',  ( 3.999999999999955147, -2.309401076758532678, -0.5000000000000004441 ) ) ;
#388=LINE ( 'NONE', #20141, #9445 ) ;
#405=VERTEX_POINT ( 'NONE', #22365 ) ;
#415=DIRECTION ( 'NONE',  ( 1.000000000000000000, -1.276756478318923119E-15, 1.239088197126283964E-15 ) ) ;
#528=CARTESIAN_POINT ( 'NONE',  ( 4.197393957002244491, 7.205051708611501750E-14, -3.503767560748914711 ) ) ;
#537=CONICAL_SURFACE ( 'NONE', #13676, 2.500000000000015543, 0.9599310885968873608 ) ;
#575=ORIENTED_EDGE ( 'NONE', *, *, #21892, .T. ) ;
#577=CARTESIAN_POINT ( 'NONE',  ( 0.000000000000000000, 0.000000000000000000, -4.000000000000000000 ) ) ;
#582=CARTESIAN_POINT ( 'NONE',  ( -4.000000000000058620, -2.309401076758546445, -3.504269196027543387 ) ) ;
#624=ORIENTED_EDGE ( 'NONE', *, *, #1356, .F. ) ;
#631=ORIENTED_EDGE ( 'NONE', *, *, #9821, .T. ) ;
#647=CARTESIAN_POINT ( 'NONE',  ( 4.211405965630437898, 2.460463115436303028, -3.751298928144580547 ) ) ;
#675=CARTESIAN_POINT ( 'NONE',  ( -4.000000000000095923, 0.9868501483902634153, -0.09357334158586104456 ) ) ;
#681=AXIS2_PLACEMENT_3D ( 'NONE', #3256, #17591, #7476 ) ;
#708=DIRECTION ( 'NONE',  ( 1.333893503340774882E-15, 2.778352770573747380E-17, 1.000000000000000000 ) ) ;
#709=FACE_OUTER_BOUND ( 'NONE', #19574, .T. ) ;
#735=CARTESIAN_POINT ( 'NONE',  ( 0.000000000000000000, 0.000000000000000000, 3.469446951953614189E-15 ) ) ;
#737=CARTESIAN_POINT ( 'NONE',  ( -4.000000000000059508, -1.539600717839031629, -3.300726591567086032 ) ) ;
#745=EDGE_CURVE ( 'NONE', #15339, #15772, #17431, .T. ) ;
#767=CARTESIAN_POINT ( 'NONE',  ( 0.000000000000000000, 0.000000000000000000, -5.000000000000000888 ) ) ;
#783=DIRECTION ( 'NONE',  ( -1.333893503340774882E-15, -2.778352770573747380E-17, -1.000000000000000000 ) ) ;
#785=ADVANCED_FACE ( 'NONE', ( #8823 ), #7065, .F. ) ;
#806=DIRECTION ( 'NONE',  ( -0.5000000000000038858, -0.8660254037844364872, -6.910079924703072041E-16 ) ) ;
#815=CARTESIAN_POINT ( 'NONE',  ( -4.000000000000058620, -2.309401076758546445, -3.433295621305388678 ) ) ;
#855=ADVANCED_FACE ( 'NONE', ( #20227 ), #18262, .T. ) ;
#864=CARTESIAN_POINT ( 'NONE',  ( 3.999999999999948042, 2.309401076758532678, -3.433295621305378020 ) ) ;
#894=ADVANCED_FACE ( 'NONE', ( #4093 ), #22410, .T. ) ;
#897=ORIENTED_EDGE ( 'NONE', *, *, #10315, .T. ) ;
#904=AXIS2_PLACEMENT_3D ( 'NONE', #1146, #20677, #16886 ) ;
#914=CARTESIAN_POINT ( 'NONE',  ( -4.000000000000095923, 0.7924765000094626810, -0.05906175389896420325 ) ) ;
#932=FACE_OUTER_BOUND ( 'NONE', #10285, .T. ) ;
#942=CIRCLE ( 'NONE', #17063, 4.000000000000023093 ) ;
#962=DIRECTION ( 'NONE',  ( 1.333893503340774882E-15, 2.778352770573747380E-17, 1.000000000000000000 ) ) ;
#965=CARTESIAN_POINT ( 'NONE',  ( 1.999999999999974021, 3.464101615137785029, 3.469446951953614189E-15 ) ) ;
#981=SHAPE_REPRESENTATION ( 'hex flange nut gradea_iso_ISO - 4161 - M5 - N', ( #22115 ), #7475 ) ;
#1032=CIRCLE ( 'NONE', #19417, 4.000000000000023093 ) ;
#1114=CARTESIAN_POINT ( 'NONE',  ( 4.203935335434104026, 1.640780671294174375, -3.598452447879221250 ) ) ;
#1125=PRODUCT_DEFINITION_CONTEXT ( 'detailed design', #2311, 'design' ) ;
#1129=EDGE_LOOP ( 'NONE', ( #13678, #18873, #19666 ) ) ;
#1146=CARTESIAN_POINT ( 'NONE',  ( 0.000000000000000000, 0.000000000000000000, 0.000000000000000000 ) ) ;
#1196=DIRECTION ( 'NONE',  ( -1.000000000000000000, 1.276756478318922725E-15, -1.333893503340766402E-15 ) ) ;
#1248=ORIENTED_EDGE ( 'NONE', *, *, #19903, .T. ) ;
#1262=ORIENTED_EDGE ( 'NONE', *, *, #10236, .T. ) ;
#1277=DIRECTION ( 'NONE',  ( -1.000000000000000000, -4.052314039881828472E-15, -1.387778780781436998E-15 ) ) ;
#1319=B_SPLINE_CURVE_WITH_KNOTS ( 'NONE', 3,
 ( #5797, #12433, #10558, #22484, #8680, #10012, #8012, #18956 ),
 .UNSPECIFIED., .F., .F.,
 ( 4, 2, 2, 4 ),
 ( 0.000000000000000000, 0.002450665683189824466, 0.003675998524784736699, 0.004901331366379648932 ),
 .UNSPECIFIED. ) ;
#1326=ORIENTED_EDGE ( 'NONE', *, *, #21892, .F. ) ;
#1356=EDGE_CURVE ( 'NONE', #8464, #7694, #5367, .T. ) ;
#1360=EDGE_CURVE ( 'NONE', #10905, #8024, #13909, .T. ) ;
#1363=ORIENTED_EDGE ( 'NONE', *, *, #15580, .F. ) ;
#1407=EDGE_LOOP ( 'NONE', ( #11723, #2320, #18772, #3662 ) ) ;
#1408=CARTESIAN_POINT ( 'NONE',  ( 4.236525694536517506, -2.416953475386506067, -3.751298745799835022 ) ) ;
#1411=FACE_OUTER_BOUND ( 'NONE', #1407, .T. ) ;
#1448=CARTESIAN_POINT ( 'NONE',  ( -3.349226789952745698, -2.685125164760777672, -0.2236248678335490125 ) ) ;
#1461=EDGE_LOOP ( 'NONE', ( #12981, #897, #19929, #16564 ) ) ;
#1473=CARTESIAN_POINT ( 'NONE',  ( 2.805705207896037390, -3.226868319750231695, -3.503898532754383233 ) ) ;
#1483=DIRECTION ( 'NONE',  ( -1.333893503340774882E-15, -2.778352770573747380E-17, -1.000000000000000000 ) ) ;
#1492=ORIENTED_EDGE ( 'NONE', *, *, #10315, .F. ) ;
#1515=CARTESIAN_POINT ( 'NONE',  ( 0.1404048886732169876, 4.699864953788106092, -3.686887068327049377 ) ) ;
#1572=EDGE_LOOP ( 'NONE', ( #18166, #10366, #15393, #12226, #22817 ) ) ;
#1586=CARTESIAN_POINT ( 'NONE',  ( -6.245004513516505540E-14, -4.862606272033144883, -3.745885042887461935 ) ) ;
#1643=CARTESIAN_POINT ( 'NONE',  ( 1.243802165048362607, -3.900692638707722093, -3.223146290109814682 ) ) ;
#1649=EDGE_LOOP ( 'NONE', ( #1326, #5753 ) ) ;
#1666=ORIENTED_EDGE ( 'NONE', *, *, #20945, .F. ) ;
#1685=CARTESIAN_POINT ( 'NONE',  ( 2.804994570502168827, 3.229033611042460006, -3.526374918436841366 ) ) ;
#1699=EDGE_LOOP ( 'NONE', ( #6758, #1938, #5310, #2617, #17509 ) ) ;
#1711=CARTESIAN_POINT ( 'NONE',  ( -4.207491450040681258, 2.029819825146493617, -3.671670828759563854 ) ) ;
#1793=CARTESIAN_POINT ( 'NONE',  ( 4.211140560182139225, 2.431303136016540911, -3.745885042887430405 ) ) ;
#1850=CARTESIAN_POINT ( 'NONE',  ( -4.141042297810708206, 2.227970268150420541, -3.687027686973645135 ) ) ;
#1854=CARTESIAN_POINT ( 'NONE',  ( -5.551115123125782702E-14, 4.618802153517065356, -0.5000000000000004441 ) ) ;
#1864=CARTESIAN_POINT ( 'NONE',  ( 2.100000000000000089, -2.611376934403532807E-15, -4.694516984716119445 ) ) ;
#1886=CARTESIAN_POINT ( 'NONE',  ( 0.6810597143191978731, 4.461075778259148805, -3.598441714920549206 ) ) ;
#1898=CARTESIAN_POINT ( 'NONE',  ( 0.000000000000000000, 0.000000000000000000, -4.974599999999998801 ) ) ;
#1903=CARTESIAN_POINT ( 'NONE',  ( 3.999999999999935163, -1.942223658245677775, -0.3516579909967328943 ) ) ;
#1913=EDGE_LOOP ( 'NONE', ( #8994, #14076, #21538, #22655 ) ) ;
#1922=DIRECTION ( 'NONE',  ( -1.333893503340774882E-15, -2.778352770573747380E-17, -1.000000000000000000 ) ) ;
#1935=SHAPE_REPRESENTATION_RELATIONSHIP ( 'NONE' , 'NONE' ,  #981, #5834 ) ;
#1938=ORIENTED_EDGE ( 'NONE', *, *, #3195, .T. ) ;
#1988=CARTESIAN_POINT ( 'NONE',  ( 4.024499207728656991, -2.323545700935616853, -3.572172305156546823 ) ) ;
#1990=SURFACE_SIDE_STYLE ('',( #8950 ) ) ;
#1995=AXIS2_PLACEMENT_3D ( 'NONE', #21572, #10948, #10730 ) ;
#2017=EDGE_CURVE ( 'NONE', #2950, #9648, #22454, .T. ) ;
#2024=CARTESIAN_POINT ( 'NONE',  ( -2.100000000000000089, 3.008176102356893744E-15, -0.2800830152838794107 ) ) ;
#2027=ORIENTED_EDGE ( 'NONE', *, *, #23005, .T. ) ;
#2033=EDGE_LOOP ( 'NONE', ( #15017, #2998, #18334, #5348 ) ) ;
#2046=CIRCLE ( 'NONE', #8063, 2.100000000000011635 ) ;
#2089=VERTEX_POINT ( 'NONE', #13283 ) ;
#2099=CARTESIAN_POINT ( 'NONE',  ( -4.000000000000052403, -2.309401076758560656, -5.000000000000000888 ) ) ;
#2147=ORIENTED_EDGE ( 'NONE', *, *, #20616, .F. ) ;
#2166=AXIS2_PLACEMENT_3D ( 'NONE', #15561, #8286, #22401 ) ;
#2185=EDGE_CURVE ( 'NONE', #11003, #11666, #6705, .T. ) ;
#2214=DIRECTION ( 'NONE',  ( 1.333893503340774882E-15, 2.778352770573747380E-17, 1.000000000000000000 ) ) ;
#2218=DIRECTION ( 'NONE',  ( -1.333893503340774882E-15, -2.778352770573747380E-17, -1.000000000000000000 ) ) ;
#2232=CARTESIAN_POINT ( 'NONE',  ( 0.3198814748697104693, 4.434118497892227673, -0.3507732604232764451 ) ) ;
#2243=CARTESIAN_POINT ( 'NONE',  ( -0.1410422978106479486, 4.700232962125154401, -3.687027686973645135 ) ) ;
#2254=CARTESIAN_POINT ( 'NONE',  ( 4.211140560182139225, 2.431303136016540911, -3.745885042887430405 ) ) ;
#2299=DIRECTION ( 'NONE',  ( 1.333893503340774882E-15, 2.778352770573747380E-17, 1.000000000000000000 ) ) ;
#2310=CARTESIAN_POINT ( 'NONE',  ( -2.100000000000000089, 3.008176102356893744E-15, -4.694516984716114116 ) ) ;
#2311=APPLICATION_CONTEXT ( 'automotive_design' ) ;
#2320=ORIENTED_EDGE ( 'NONE', *, *, #20768, .T. ) ;
#2366=CIRCLE ( 'NONE', #5393, 2.500000000000015543 ) ;
#2382=VERTEX_POINT ( 'NONE', #21403 ) ;
#2404=PLANE ( 'NONE',  #19448 ) ;
#2409=CARTESIAN_POINT ( 'NONE',  ( 0.000000000000000000, 0.000000000000000000, 3.469446951953614189E-15 ) ) ;
#2445=ORIENTED_EDGE ( 'NONE', *, *, #7108, .T. ) ;
#2475=CARTESIAN_POINT ( 'NONE',  ( -5.560781378645605066, 7.099763649701009246E-15, -4.000000000000007994 ) ) ;
#2514=CYLINDRICAL_SURFACE ( 'NONE', #17562, 2.100000000000011635 ) ;
#2569=DIRECTION ( 'NONE',  ( -1.333893503340774882E-15, -2.778352770573747380E-17, -1.000000000000000000 ) ) ;
#2617=ORIENTED_EDGE ( 'NONE', *, *, #7108, .F. ) ;
#2655=CARTESIAN_POINT ( 'NONE',  ( 0.6666666666666630769, 4.233901974057274309, -3.300726591567085144 ) ) ;
#2682=EDGE_CURVE ( 'NONE', #8464, #9707, #10899, .T. ) ;
#2779=LINE ( 'NONE', #12171, #21502 ) ;
#2837=CARTESIAN_POINT ( 'NONE',  ( -6.245004513516505540E-14, -4.862606272033144883, -3.745885042887461935 ) ) ;
#2862=CARTESIAN_POINT ( 'NONE',  ( 4.197478902586910365, -0.8524102783748742640, -3.505063281295481392 ) ) ;
#2864=CARTESIAN_POINT ( 'NONE',  ( -1.040834085586084257E-13, 4.862606272033151100, -3.745885042887441063 ) ) ;
#2871=PLANE ( 'NONE',  #13409 ) ;
#2879=VECTOR ( 'NONE', #15212, 1000.000000000000114 ) ;
#2886=DIRECTION ( 'NONE',  ( 1.333893503340774882E-15, 2.778352770573747380E-17, 1.000000000000000000 ) ) ;
#2909=PRODUCT ( 'hex flange nut gradea_iso_ISO - 4161 - M5 - N', 'hex flange nut gradea_iso_ISO - 4161 - M5 - N', '', ( #7536 ) ) ;
#2926=AXIS2_PLACEMENT_3D ( 'NONE', #735, #6146, #9906 ) ;
#2950=VERTEX_POINT ( 'NONE', #20058 ) ;
#2954=CARTESIAN_POINT ( 'NONE',  ( 3.679171394225956515, 2.494631558665878046, -0.3503314178412145763 ) ) ;
#2963=DIRECTION ( 'NONE',  ( 0.000000000000000000, 0.000000000000000000, 1.000000000000000000 ) ) ;
#2971=ORIENTED_EDGE ( 'NONE', *, *, #21187, .F. ) ;
#2978=AXIS2_PLACEMENT_3D ( 'NONE', #20209, #9489, #16529 ) ;
#2985=CARTESIAN_POINT ( 'NONE',  ( -2.344047193898689763, -3.265465875126513318, -7.162087085508733993E-14 ) ) ;
#2998=ORIENTED_EDGE ( 'NONE', *, *, #16403, .F. ) ;
#3008=FACE_OUTER_BOUND ( 'NONE', #1129, .T. ) ;
#3009=CARTESIAN_POINT ( 'NONE',  ( 1.393927851585456290, -4.043713361053605126, -3.526374918436861350 ) ) ;
#3014=CARTESIAN_POINT ( 'NONE',  ( -4.000000000000095035, 1.563622288139215888, -0.2253451193528957786 ) ) ;
#3070=CARTESIAN_POINT ( 'NONE',  ( 6.248040462138590701E-13, -4.796980096169678021, -3.721999068284442380 ) ) ;
#3087=ORIENTED_EDGE ( 'NONE', *, *, #10236, .F. ) ;
#3128=EDGE_CURVE ( 'NONE', #15881, #7096, #4700, .T. ) ;
#3129=CARTESIAN_POINT ( 'NONE',  ( 0.6937372685066356404, -4.453844082567806062, -3.610536846335917982 ) ) ;
#3133=CARTESIAN_POINT ( 'NONE',  ( 0.000000000000000000, 0.000000000000000000, -4.000000000000000000 ) ) ;
#3139=DIRECTION ( 'NONE',  ( -1.000000000000000000, 1.276756478318923119E-15, -1.387778780781436998E-15 ) ) ;
#3141=CIRCLE ( 'NONE', #1995, 0.5155456020628804703 ) ;
#3195=EDGE_CURVE ( 'NONE', #9560, #8464, #13662, .T. ) ;
#3250=CARTESIAN_POINT ( 'NONE',  ( -1.391697335622858356, -4.043246145443450068, -3.503898532754396555 ) ) ;
#3256=CARTESIAN_POINT ( 'NONE',  ( 0.000000000000000000, 0.000000000000000000, 3.469446951953614189E-15 ) ) ;
#3299=CARTESIAN_POINT ( 'NONE',  ( 3.999999999999955147, -2.309401076758532678, -0.5000000000000004441 ) ) ;
#3309=CARTESIAN_POINT ( 'NONE',  ( 0.3208286057739342945, -4.433571671609761289, -0.3503314178413123869 ) ) ;
#3314=LINE ( 'NONE', #17770, #5546 ) ;
#3320=ORIENTED_EDGE ( 'NONE', *, *, #15580, .T. ) ;
#3348=CARTESIAN_POINT ( 'NONE',  ( -3.999999999998653966, -1.658469974638416167, -3.531532913076295355 ) ) ;
#3369=ADVANCED_FACE ( 'NONE', ( #22349 ), #11504, .F. ) ;
#3403=CARTESIAN_POINT ( 'NONE',  ( -1.040834085586084257E-13, 4.862606272033151100, -3.745885042887441063 ) ) ;
#3409=B_SPLINE_CURVE_WITH_KNOTS ( 'NONE', 3,
 ( #8006, #18597, #6365, #16923, #22124 ),
 .UNSPECIFIED., .F., .F.,
 ( 4, 1, 4 ),
 ( 0.000000000000000000, 0.002309401076758508826, 0.004618802153517017652 ),
 .UNSPECIFIED. ) ;
#3412=CARTESIAN_POINT ( 'NONE',  ( 0.5469614295417839500, -4.303013824935142395, -3.535263753545104581 ) ) ;
#3419=DIRECTION ( 'NONE',  ( 1.333893503340774882E-15, 2.778352770573747380E-17, 1.000000000000000000 ) ) ;
#3434=ORIENTED_EDGE ( 'NONE', *, *, #745, .F. ) ;
#3452=CARTESIAN_POINT ( 'NONE',  ( -4.203934362469490260, -1.640673743454793776, -3.598432614607018465 ) ) ;
#3482=FILL_AREA_STYLE_COLOUR ( '', #9353 ) ;
#3628=CARTESIAN_POINT ( 'NONE',  ( 0.02448733951232850634, 4.877042772274765348, -3.751161874094034232 ) ) ;
#3638=B_SPLINE_CURVE_WITH_KNOTS ( 'NONE', 3,
 ( #8768, #14522, #17945, #17833, #1711, #293 ),
 .UNSPECIFIED., .F., .F.,
 ( 4, 2, 4 ),
 ( 0.002452478801916411870, 0.003676905084148028666, 0.004901331366379645463 ),
 .UNSPECIFIED. ) ;
#3640=DIRECTION ( 'NONE',  ( 1.333893503340774882E-15, 2.778352770573747380E-17, 1.000000000000000000 ) ) ;
#3662=ORIENTED_EDGE ( 'NONE', *, *, #15275, .F. ) ;
#3674=DIRECTION ( 'NONE',  ( 1.333893503340774882E-15, 2.778352770573747380E-17, 1.000000000000000000 ) ) ;
#3722=CARTESIAN_POINT ( 'NONE',  ( -1.144235203016779945, -3.958177651039131550, -0.09382832055450740505 ) ) ;
#3735=EDGE_CURVE ( 'NONE', #405, #22849, #13493, .T. ) ;
#3738=DIRECTION ( 'NONE',  ( 1.333893503340774882E-15, 2.778352770573747380E-17, 1.000000000000000000 ) ) ;
#3754=CARTESIAN_POINT ( 'NONE',  ( 4.154306624730736530, -2.398490048085659243, -3.721999068284422840 ) ) ;
#3761=EDGE_CURVE ( 'NONE', #2382, #22002, #18431, .T. ) ;
#3781=CARTESIAN_POINT ( 'NONE',  ( 3.999999999999955147, -2.309401076758539784, -5.000000000000000888 ) ) ;
#3809=FACE_BOUND ( 'NONE', #1649, .T. ) ;
#3912=CIRCLE ( 'NONE', #7687, 2.100000000000011635 ) ;
#3920=ORIENTED_EDGE ( 'NONE', *, *, #2017, .F. ) ;
#3930=CIRCLE ( 'NONE', #9209, 4.000000000000023093 ) ;
#4012=CARTESIAN_POINT ( 'NONE',  ( 4.203833317240822431, 1.627343821129635382, -3.597273115243896591 ) ) ;
#4031=ORIENTED_EDGE ( 'NONE', *, *, #1360, .F. ) ;
#4053=ADVANCED_FACE ( 'NONE', ( #9009 ), #14416, .T. ) ;
#4059=ADVANCED_FACE ( 'NONE', ( #19359 ), #4799, .T. ) ;
#4093=FACE_OUTER_BOUND ( 'NONE', #17455, .T. ) ;
#4107=AXIS2_PLACEMENT_3D ( 'NONE', #6544, #4531, #17339 ) ;
#4109=ADVANCED_FACE ( 'NONE', ( #20176, #4272 ), #2404, .T. ) ;
#4156=ADVANCED_FACE ( 'NONE', ( #19947 ), #2514, .F. ) ;
#4176=CARTESIAN_POINT ( 'NONE',  ( -1.828356344711745018, -3.563200125723226197, -6.548411715222995921E-14 ) ) ;
#4183=EDGE_CURVE ( 'NONE', #9648, #19280, #16507, .T. ) ;
#4208=CARTESIAN_POINT ( 'NONE',  ( 0.000000000000000000, 0.000000000000000000, -5.000000000000000888 ) ) ;
#4236=ADVANCED_FACE ( 'NONE', ( #19210 ), #11932, .T. ) ;
#4250=( BOUNDED_SURFACE ( )  B_SPLINE_SURFACE ( 3, 2, ( 
 ( #12237, #10719, #14258 ),
 ( #7324, #19904, #21673 ),
 ( #19547, #12475, #5553 ),
 ( #19425, #21560, #12719 ),
 ( #12600, #19785, #1886 ),
 ( #9070, #2243, #15046 ) ),
 .UNSPECIFIED., .F., .F., .T. ) 
 B_SPLINE_SURFACE_WITH_KNOTS ( ( 4, 2, 4 ),
 ( 3, 3 ),
 ( 0.02032853247518126225, 0.02278863295364821906, 0.02524873343211517240 ),
 ( 0.000000000000000000, 1.000000000000000000 ),
 .UNSPECIFIED. ) 
 GEOMETRIC_REPRESENTATION_ITEM ( )  RATIONAL_B_SPLINE_SURFACE ( (
 ( 1.000000000000000000, 0.8047781615896839602, 1.000000000000000000),
 ( 1.000000000000000000, 0.8123767586289271092, 1.000000000000000000),
 ( 1.000000000000000000, 0.8190662415564389232, 1.000000000000000000),
 ( 1.000000000000000000, 0.8192361015669027413, 1.000000000000000000),
 ( 1.000000000000000000, 0.8126135807103893605, 1.000000000000000000),
 ( 1.000000000000000000, 0.8047712338318578906, 1.000000000000000000) ) ) 
 REPRESENTATION_ITEM ( '' )  SURFACE ( )  );
#4272=FACE_OUTER_BOUND ( 'NONE', #8748, .T. ) ;
#4274=VECTOR ( 'NONE', #15899, 1000.000000000000000 ) ;
#4277=DIRECTION ( 'NONE',  ( -1.000000000000000000, 1.276756478318922922E-15, 1.333893503340774882E-15 ) ) ;
#4329=CARTESIAN_POINT ( 'NONE',  ( -5.551115123125782702E-14, 4.618802153517065356, -0.5000000000000004441 ) ) ;
#4344=LINE ( 'NONE', #2475, #7189 ) ;
#4356=CARTESIAN_POINT ( 'NONE',  ( -4.000000000000058620, -2.309401076758546445, -3.433295621305388678 ) ) ;
#4448=PRODUCT_DEFINITION ( 'UNKNOWN', '', #15765, #1125 ) ;
#4475=CARTESIAN_POINT ( 'NONE',  ( -6.763542839912098701E-14, -4.647091401871226601, -3.572172305156534833 ) ) ;
#4483=CARTESIAN_POINT ( 'NONE',  ( -4.000000000000100364, 2.309401076758546445, -3.433295621305381573 ) ) ;
#4492=ORIENTED_EDGE ( 'NONE', *, *, #6913, .T. ) ;
#4499=AXIS2_PLACEMENT_3D ( 'NONE', #7468, #1922, #11322 ) ;
#4509=CARTESIAN_POINT ( 'NONE',  ( 3.999999999999981792, 2.472263674411438128, -3.687027874309864561 ) ) ;
#4524=EDGE_LOOP ( 'NONE', ( #2027, #10750, #3434 ) ) ;
#4531=DIRECTION ( 'NONE',  ( -1.333893503340774882E-15, -2.778352770573747380E-17, -1.000000000000000000 ) ) ;
#4591=DIRECTION ( 'NONE',  ( 1.333893503340774882E-15, 2.778352770573747380E-17, 1.000000000000000000 ) ) ;
#4595=AXIS2_PLACEMENT_3D ( 'NONE', #14437, #21622, #7265 ) ;
#4597=ORIENTED_EDGE ( 'NONE', *, *, #11360, .T. ) ;
#4620=CARTESIAN_POINT ( 'NONE',  ( 3.999999999999980904, 2.512223110932565007, -3.469391141908806819 ) ) ;
#4627=LINE ( 'NONE', #18868, #14946 ) ;
#4636=VECTOR ( 'NONE', #22715, 1000.000000000000000 ) ;
#4653=EDGE_CURVE ( 'NONE', #15514, #6303, #1319, .T. ) ;
#4700=B_SPLINE_CURVE_WITH_KNOTS ( 'NONE', 3,
 ( #12344, #16214, #21309, #15988, #11047, #12812 ),
 .UNSPECIFIED., .F., .F.,
 ( 4, 2, 4 ),
 ( 0.003358874760055556661, 0.004541967308452141486, 0.005725059856848725010 ),
 .UNSPECIFIED. ) ;
#4702=ORIENTED_EDGE ( 'NONE', *, *, #20170, .F. ) ;
#4730=B_SPLINE_CURVE_WITH_KNOTS ( 'NONE', 3,
 ( #14222, #14100, #6937, #9039, #14329, #1854 ),
 .UNSPECIFIED., .F., .F.,
 ( 4, 2, 4 ),
 ( 0.002365888236228012864, 0.003551327329835094089, 0.004736766423442174447 ),
 .UNSPECIFIED. ) ;
#4748=EDGE_LOOP ( 'NONE', ( #5282, #13496, #12472, #6941 ) ) ;
#4763=CARTESIAN_POINT ( 'NONE',  ( 3.511755186886688307, -2.826662030176431362, -3.597382984111577642 ) ) ;
#4794=DIRECTION ( 'NONE',  ( -1.000000000000000000, 1.399221158233660042E-15, 0.000000000000000000 ) ) ;
#4799=CONICAL_SURFACE ( 'NONE', #681, 4.000000000000022204, 0.8911886515913840512 ) ;
#4839=UNCERTAINTY_MEASURE_WITH_UNIT (LENGTH_MEASURE( 1.000000000000000082E-05 ), #16167, 'distance_accuracy_value', 'NONE');
#4845=CARTESIAN_POINT ( 'NONE',  ( -4.203833317240987633, -1.627343821129589418, -3.597273115243885044 ) ) ;
#4848=CARTESIAN_POINT ( 'NONE',  ( 5.560781378645605066, -6.418764338089353846E-15, -3.999999999999992450 ) ) ;
#4852=DIRECTION ( 'NONE',  ( 1.000000000000000000, -1.276756478318922922E-15, 1.342094922251465017E-15 ) ) ;
#4877=B_SPLINE_CURVE_WITH_KNOTS ( 'NONE', 3,
 ( #528, #16498, #14636, #14744, #22045, #5706 ),
 .UNSPECIFIED., .F., .F.,
 ( 4, 2, 4 ),
 ( 0.002452478801916372839, 0.003676905084148008283, 0.004901331366379643728 ),
 .UNSPECIFIED. ) ;
#4932=CIRCLE ( 'NONE', #17716, 5.560781378645605066 ) ;
#4942=LINE ( 'NONE', #12111, #9324 ) ;
#4943=CARTESIAN_POINT ( 'NONE',  ( 0.000000000000000000, 0.000000000000000000, 0.000000000000000000 ) ) ;
#4980=ORIENTED_EDGE ( 'NONE', *, *, #20945, .T. ) ;
#5010=CARTESIAN_POINT ( 'NONE',  ( 4.211140560182194292, -2.431303136016568889, -3.745885042887441063 ) ) ;
#5048=ORIENTED_EDGE ( 'NONE', *, *, #7234, .T. ) ;
#5051=ADVANCED_FACE ( 'NONE', ( #22662 ), #13642, .T. ) ;
#5052=B_SPLINE_CURVE_WITH_KNOTS ( 'NONE', 3,
 ( #6623, #2985, #22629, #1448, #8622, #10156 ),
 .UNSPECIFIED., .F., .F.,
 ( 4, 2, 4 ),
 ( 0.002365888236228034115, 0.003551327329835107967, 0.004736766423442182253 ),
 .UNSPECIFIED. ) ;
#5053=CARTESIAN_POINT ( 'NONE',  ( 1.257172072275264174, -3.892973519171180730, -3.433252694550784856 ) ) ;
#5064=CARTESIAN_POINT ( 'NONE',  ( -9.714451465470119729E-14, -4.618802153517051146, -0.5000000000000004441 ) ) ;
#5084=DIRECTION ( 'NONE',  ( 1.333893503340774882E-15, 2.778352770573747380E-17, 1.000000000000000000 ) ) ;
#5102=CARTESIAN_POINT ( 'NONE',  ( -9.714451465470119729E-14, -4.618802153517051146, -0.5000000000000004441 ) ) ;
#5158=CARTESIAN_POINT ( 'NONE',  ( -2.807080416177946347, 3.225969019225889856, -3.502507215260549867 ) ) ;
#5184=CARTESIAN_POINT ( 'NONE',  ( 4.000000000000007994, 8.673617379884035472E-16, -3.142992957459231462 ) ) ;
#5187=FILL_AREA_STYLE_COLOUR ( '', #11535 ) ;
#5202=FACE_OUTER_BOUND ( 'NONE', #19169, .T. ) ;
#5226=CARTESIAN_POINT ( 'NONE',  ( -4.000000000000102141, 2.511478553582021433, -3.469254451724788524 ) ) ;
#5249=CARTESIAN_POINT ( 'NONE',  ( 0.1410422978105614067, -4.700232962125169500, -3.687027686973649132 ) ) ;
#5282=ORIENTED_EDGE ( 'NONE', *, *, #2185, .F. ) ;
#5306=DIRECTION ( 'NONE',  ( 1.000000000000000000, 0.000000000000000000, 0.000000000000000000 ) ) ;
#5310=ORIENTED_EDGE ( 'NONE', *, *, #21065, .T. ) ;
#5318=DIRECTION ( 'NONE',  ( -1.000000000000000000, 1.276756478318923119E-15, -1.333893503340766797E-15 ) ) ;
#5348=ORIENTED_EDGE ( 'NONE', *, *, #368, .F. ) ;
#5362=CARTESIAN_POINT ( 'NONE',  ( -4.024497503033621193, 2.323544716729374571, -3.572167766733397976 ) ) ;
#5367=B_SPLINE_CURVE_WITH_KNOTS ( 'NONE', 3,
 ( #22272, #6168, #11559, #6278, #8501, #10150 ),
 .UNSPECIFIED., .F., .F.,
 ( 4, 2, 4 ),
 ( 0.000000000000000000, 0.0002095117440854730941, 0.0004190234881709461881 ),
 .UNSPECIFIED. ) ;
#5393=AXIS2_PLACEMENT_3D ( 'NONE', #21794, #7771, #16808 ) ;
#5403=CARTESIAN_POINT ( 'NONE',  ( 0.000000000000000000, 0.000000000000000000, -4.484454397937119197 ) ) ;
#5436=EDGE_LOOP ( 'NONE', ( #12421, #18694, #19455, #8267 ) ) ;
#5443=DIRECTION ( 'NONE',  ( 1.333893503340774882E-15, 2.778352770573747380E-17, 1.000000000000000000 ) ) ;
#5481=DIRECTION ( 'NONE',  ( 0.5000000000000047740, 0.8660254037844359321, 6.910079924703084860E-16 ) ) ;
#5517=ORIENTED_EDGE ( 'NONE', *, *, #20768, .F. ) ;
#5546=VECTOR ( 'NONE', #6005, 1000.000000000000000 ) ;
#5547=SHAPE_DEFINITION_REPRESENTATION ( #15290, #981 ) ;
#5553=CARTESIAN_POINT ( 'NONE',  ( 2.836893136758258382, 3.208949435746023315, -3.505054077164891257 ) ) ;
#5558=CARTESIAN_POINT ( 'NONE',  ( -6.245004513516505540E-14, -4.862606272033144883, -3.745885042887461935 ) ) ;
#5559=CARTESIAN_POINT ( 'NONE',  ( 1.999999999999974021, 3.464101615137785029, 3.469446951953614189E-15 ) ) ;
#5575=ORIENTED_EDGE ( 'NONE', *, *, #14407, .F. ) ;
#5594=CARTESIAN_POINT ( 'NONE',  ( -3.333333333333390325, -2.694301256218301965, -3.300726591567088253 ) ) ;
#5620=CARTESIAN_POINT ( 'NONE',  ( -1.312671235360486133, -3.860931062424260762, -0.05923475698275939422 ) ) ;
#5642=DIRECTION ( 'NONE',  ( -1.000000000000000000, 1.276756478318923119E-15, -1.403805528459192781E-15 ) ) ;
#5674=ADVANCED_FACE ( 'NONE', ( #11648 ), #6703, .T. ) ;
#5683=CARTESIAN_POINT ( 'NONE',  ( 4.197393957002244491, 7.205051708611501750E-14, -3.503767560748914711 ) ) ;
#5706=CARTESIAN_POINT ( 'NONE',  ( 4.211140560182194292, -2.431303136016568889, -3.745885042887441063 ) ) ;
#5716=DIRECTION ( 'NONE',  ( -1.000000000000000000, 1.276756478318922922E-15, -1.333893503340766797E-15 ) ) ;
#5734=CARTESIAN_POINT ( 'NONE',  ( -9.714451465470119729E-14, -4.618802153517051146, -0.5000000000000004441 ) ) ;
#5743=AXIS2_PLACEMENT_3D ( 'NONE', #17132, #20571, #1277 ) ;
#5753=ORIENTED_EDGE ( 'NONE', *, *, #6708, .F. ) ;
#5762=CARTESIAN_POINT ( 'NONE',  ( -2.893953949542924385E-14, 4.736522675502212287, -3.681124513963636602 ) ) ;
#5767=DIRECTION ( 'NONE',  ( 1.000000000000000000, -1.276756478318923119E-15, 1.342345546886807594E-15 ) ) ;
#5797=CARTESIAN_POINT ( 'NONE',  ( -4.211140560182312420, 2.431303136016568889, -3.745885042887433958 ) ) ;
#5834=ADVANCED_BREP_SHAPE_REPRESENTATION ( '', ( #21055, #22115 ), #7475 ) ;
#5873=DIRECTION ( 'NONE',  ( -1.000000000000000000, 1.276756478318922725E-15, -1.333893503340766402E-15 ) ) ;
#5931=LINE ( 'NONE', #8353, #4636 ) ;
#6005=DIRECTION ( 'NONE',  ( 1.333893503340774882E-15, 2.778352770573747380E-17, 1.000000000000000000 ) ) ;
#6080=CARTESIAN_POINT ( 'NONE',  ( -4.000000000000095035, 1.941961291383484278, -0.3515519931180789981 ) ) ;
#6101=DIRECTION ( 'NONE',  ( -1.333893503340774882E-15, -2.778352770573747380E-17, -1.000000000000000000 ) ) ;
#6146=DIRECTION ( 'NONE',  ( 1.333893503340774882E-15, 2.778352770573747380E-17, 1.000000000000000000 ) ) ;
#6166=ORIENTED_EDGE ( 'NONE', *, *, #19879, .T. ) ;
#6168=CARTESIAN_POINT ( 'NONE',  ( 3.999999999999948042, 2.309401076758532678, -3.504271511726787747 ) ) ;
#6173=CARTESIAN_POINT ( 'NONE',  ( 3.999999999999976019, -1.700175430507228969, -3.320327275038315484 ) ) ;
#6183=ORIENTED_EDGE ( 'NONE', *, *, #17280, .T. ) ;
#6188=B_SPLINE_CURVE_WITH_KNOTS ( 'NONE', 3,
 ( #20059, #14299, #21487, #5362, #16853, #20643 ),
 .UNSPECIFIED., .F., .F.,
 ( 4, 2, 4 ),
 ( -3.640115492456156008E-06, 0.0002066546034006130211, 0.0004169493222936822025 ),
 .UNSPECIFIED. ) ;
#6247=PLANE ( 'NONE',  #22299 ) ;
#6266=ORIENTED_EDGE ( 'NONE', *, *, #186, .F. ) ;
#6278=CARTESIAN_POINT ( 'NONE',  ( 4.101954839143033382, 2.368264730582954947, -3.681130640444268298 ) ) ;
#6303=VERTEX_POINT ( 'NONE', #3403 ) ;
#6313=CARTESIAN_POINT ( 'NONE',  ( 6.938893903907228378E-15, 4.618802153517023612, -3.433295621305385126 ) ) ;
#6333=CARTESIAN_POINT ( 'NONE',  ( -4.000000000000052403, -2.309401076758560656, -5.000000000000000888 ) ) ;
#6365=CARTESIAN_POINT ( 'NONE',  ( 1.999999999999944045, -3.464101615137820112, -3.142992957459231462 ) ) ;
#6403=CARTESIAN_POINT ( 'NONE',  ( 3.999999999999975131, -2.471525695159832559, -3.686886880705775305 ) ) ;
#6463=B_SPLINE_CURVE_WITH_KNOTS ( 'NONE', 3,
 ( #7520, #21869, #5762, #12927, #20105, #10577 ),
 .UNSPECIFIED., .F., .F.,
 ( 4, 2, 4 ),
 ( -3.640115492385053097E-06, 0.0002066546034006847140, 0.0004169493222937545188 ),
 .UNSPECIFIED. ) ;
#6486=B_SPLINE_CURVE_WITH_KNOTS ( 'NONE', 3,
 ( #11627, #22814, #8229, #11744, #15268 ),
 .UNSPECIFIED., .F., .F.,
 ( 4, 1, 4 ),
 ( 0.000000000000000000, 0.002309401076758508826, 0.004618802153517017652 ),
 .UNSPECIFIED. ) ;
#6500=ORIENTED_EDGE ( 'NONE', *, *, #18462, .T. ) ;
#6515=FACE_OUTER_BOUND ( 'NONE', #20381, .T. ) ;
#6544=CARTESIAN_POINT ( 'NONE',  ( 0.000000000000000000, 0.000000000000000000, 3.469446951953614189E-15 ) ) ;
#6591=VERTEX_POINT ( 'NONE', #2024 ) ;
#6623=CARTESIAN_POINT ( 'NONE',  ( -2.000000000000119904, -3.464101615137792134, -1.040834085586084257E-14 ) ) ;
#6629=FACE_OUTER_BOUND ( 'NONE', #1572, .T. ) ;
#6664=( GEOMETRIC_REPRESENTATION_CONTEXT ( 3 ) GLOBAL_UNCERTAINTY_ASSIGNED_CONTEXT ( ( #18971 ) ) GLOBAL_UNIT_ASSIGNED_CONTEXT ( ( #16343, #19411, #17647 ) ) REPRESENTATION_CONTEXT ( 'NONE', 'WORKASPACE' ) );
#6703=CONICAL_SURFACE ( 'NONE', #20983, 4.000000000000022204, 0.8911886515913840512 ) ;
#6705=B_SPLINE_CURVE_WITH_KNOTS ( 'NONE', 3,
 ( #11274, #9754, #11042, #18231, #582, #815 ),
 .UNSPECIFIED., .F., .F.,
 ( 4, 2, 4 ),
 ( -3.640115492440753560E-06, 0.0002066546034006306394, 0.0004169493222937020434 ),
 .UNSPECIFIED. ) ;
#6708=EDGE_CURVE ( 'NONE', #20837, #7256, #22828, .T. ) ;
#6736=DIRECTION ( 'NONE',  ( 0.9396926207859150892, -1.094182011322127520E-15, -0.3420201433256501722 ) ) ;
#6758=ORIENTED_EDGE ( 'NONE', *, *, #18052, .F. ) ;
#6764=CARTESIAN_POINT ( 'NONE',  ( 4.211140560182194292, -2.431303136016568889, -3.745885042887441063 ) ) ;
#6769=DIRECTION ( 'NONE',  ( -0.8191520442889964615, 1.029921702463447212E-15, -0.5735764363510394981 ) ) ;
#6780=PRESENTATION_STYLE_ASSIGNMENT (( #19832 ) ) ;
#6782=CARTESIAN_POINT ( 'NONE',  ( 0.000000000000000000, 0.000000000000000000, 3.469446951953614189E-15 ) ) ;
#6809=CARTESIAN_POINT ( 'NONE',  ( -2.687328764639671075, 3.067272167851270215, -0.05923475698270320999 ) ) ;
#6833=CARTESIAN_POINT ( 'NONE',  ( 4.101954839143034270, -2.368264730582960720, -3.681130640444259861 ) ) ;
#6848=CARTESIAN_POINT ( 'NONE',  ( -4.197393957002394593, -7.172049766556752605E-14, -3.503767560748959120 ) ) ;
#6883=EDGE_LOOP ( 'NONE', ( #16033, #2971, #8847, #16721 ) ) ;
#6888=CARTESIAN_POINT ( 'NONE',  ( 1.747541505913256188, -3.837784562140331257, -3.503702292528931395 ) ) ;
#6905=CARTESIAN_POINT ( 'NONE',  ( 4.211140560182139225, 2.431303136016540911, -3.745885042887430405 ) ) ;
#6911=VERTEX_POINT ( 'NONE', #21077 ) ;
#6913=EDGE_CURVE ( 'NONE', #13336, #18554, #4942, .T. ) ;
#6932=CARTESIAN_POINT ( 'NONE',  ( -1.243802165050142072, 3.900692638706738435, -3.223146290109823120 ) ) ;
#6937=CARTESIAN_POINT ( 'NONE',  ( -1.317756351988384145, 3.857995168970181687, -0.04852650426600636085 ) ) ;
#6941=ORIENTED_EDGE ( 'NONE', *, *, #10131, .F. ) ;
#6947=CARTESIAN_POINT ( 'NONE',  ( 1.999999999999953149, -3.464101615137771262, 0.000000000000000000 ) ) ;
#6976=EDGE_LOOP ( 'NONE', ( #1363, #12770, #16688, #12038, #18468 ) ) ;
#6991=CARTESIAN_POINT ( 'NONE',  ( -4.000000000000058620, -2.309401076758546445, -3.433295621305388678 ) ) ;
#7026=( LENGTH_UNIT ( ) NAMED_UNIT ( * ) SI_UNIT ( .MILLI., .METRE. ) );
#7040=VECTOR ( 'NONE', #6736, 1000.000000000000114 ) ;
#7051=CARTESIAN_POINT ( 'NONE',  ( -2.712762565638113355, 3.052587955998298241, -3.430618716626830267 ) ) ;
#7065=PLANE ( 'NONE',  #8136 ) ;
#7075=CARTESIAN_POINT ( 'NONE',  ( 1.317756351988315533, -3.857995168970278499, -0.04852650426606291284 ) ) ;
#7096=VERTEX_POINT ( 'NONE', #8954 ) ;
#7108=EDGE_CURVE ( 'NONE', #22298, #13467, #214, .T. ) ;
#7116=CARTESIAN_POINT ( 'NONE',  ( -4.211405944401508172, -2.460460786169425429, -3.751298493805527823 ) ) ;
#7140=CARTESIAN_POINT ( 'NONE',  ( -1.274258131565020324, -3.883108878240975947, -3.220599429844259731 ) ) ;
#7189=VECTOR ( 'NONE', #8010, 1000.000000000000000 ) ;
#7212=EDGE_CURVE ( 'NONE', #9707, #17275, #22815, .T. ) ;
#7234=EDGE_CURVE ( 'NONE', #20801, #10484, #20118, .T. ) ;
#7235=ORIENTED_EDGE ( 'NONE', *, *, #174, .T. ) ;
#7244=CARTESIAN_POINT ( 'NONE',  ( -3.861362476283353384, -2.629030857716048608, -3.671615880910375385 ) ) ;
#7247=CARTESIAN_POINT ( 'NONE',  ( -1.287237434361804045, -3.875615274277503186, -3.430618716626840925 ) ) ;
#7256=VERTEX_POINT ( 'NONE', #8111 ) ;
#7265=DIRECTION ( 'NONE',  ( 1.000000000000000000, -1.276756478318923119E-15, 1.387778780781436998E-15 ) ) ;
#7284=CARTESIAN_POINT ( 'NONE',  ( -3.522875095020107317, 2.820352903224537577, -3.598441714920560752 ) ) ;
#7305=CARTESIAN_POINT ( 'NONE',  ( -5.551115123125782702E-14, 4.618802153517065356, -0.5000000000000004441 ) ) ;
#7318=ORIENTED_EDGE ( 'NONE', *, *, #186, .T. ) ;
#7324=CARTESIAN_POINT ( 'NONE',  ( 3.472371940586146177, 2.614027278893112261, -3.320322319202220651 ) ) ;
#7350=ORIENTED_EDGE ( 'NONE', *, *, #17893, .T. ) ;
#7354=CARTESIAN_POINT ( 'NONE',  ( -2.081668171172168513E-14, 4.618802153517051146, 0.000000000000000000 ) ) ;
#7365=ADVANCED_FACE ( 'NONE', ( #16193 ), #13100, .T. ) ;
#7468=CARTESIAN_POINT ( 'NONE',  ( 0.000000000000000000, 0.000000000000000000, 3.469446951953614189E-15 ) ) ;
#7475=( GEOMETRIC_REPRESENTATION_CONTEXT ( 3 ) GLOBAL_UNCERTAINTY_ASSIGNED_CONTEXT ( ( #13787 ) ) GLOBAL_UNIT_ASSIGNED_CONTEXT ( ( #7026, #8896, #21494 ) ) REPRESENTATION_CONTEXT ( 'NONE', 'WORKASPACE' ) );
#7476=DIRECTION ( 'NONE',  ( -1.000000000000000000, 1.276756478318922725E-15, -1.333893503340766402E-15 ) ) ;
#7520=CARTESIAN_POINT ( 'NONE',  ( -1.040834085586084257E-13, 4.862606272033151100, -3.745885042887441063 ) ) ;
#7536=PRODUCT_CONTEXT ( 'NONE', #17783, 'mechanical' ) ;
#7553=DIRECTION ( 'NONE',  ( 1.000000000000000000, -1.276756478318923119E-15, 1.387778780781436998E-15 ) ) ;
#7577=CARTESIAN_POINT ( 'NONE',  ( -2.000000000000043077, -3.464101615137785917, -3.142992957459260772 ) ) ;
#7592=ORIENTED_EDGE ( 'NONE', *, *, #21065, .F. ) ;
#7598=CIRCLE ( 'NONE', #14727, 0.5155456020628804703 ) ;
#7652=VERTEX_POINT ( 'NONE', #15363 ) ;
#7672=DIRECTION ( 'NONE',  ( 0.8191520442889970166, -9.614764631795313332E-16, -0.5735764363510387209 ) ) ;
#7687=AXIS2_PLACEMENT_3D ( 'NONE', #9719, #783, #7944 ) ;
#7688=ORIENTED_EDGE ( 'NONE', *, *, #17678, .T. ) ;
#7694=VERTEX_POINT ( 'NONE', #6905 ) ;
#7702=CARTESIAN_POINT ( 'NONE',  ( -3.510273485745384558, -2.827716139362705938, -3.610536846335915317 ) ) ;
#7771=DIRECTION ( 'NONE',  ( 1.333893503340774882E-15, 2.778352770573747380E-17, 1.000000000000000000 ) ) ;
#7875=ADVANCED_FACE ( 'NONE', ( #16627 ), #9359, .T. ) ;
#7888=DIRECTION ( 'NONE',  ( -0.5000000000000014433, 0.8660254037844378194, -6.428855108704672838E-16 ) ) ;
#7925=CARTESIAN_POINT ( 'NONE',  ( 4.211399257449685685, -2.459727064652556194, -3.751161691472421733 ) ) ;
#7944=DIRECTION ( 'NONE',  ( 1.000000000000000000, -1.276756478318923119E-15, 1.342345546886807594E-15 ) ) ;
#7967=ORIENTED_EDGE ( 'NONE', *, *, #4183, .T. ) ;
#8006=CARTESIAN_POINT ( 'NONE',  ( -6.938893903907228378E-14, -4.618802153517121312, -3.433295621305409107 ) ) ;
#8010=DIRECTION ( 'NONE',  ( -0.9396926207859144231, 1.190256115088894218E-15, -0.3420201433256521706 ) ) ;
#8012=CARTESIAN_POINT ( 'NONE',  ( -0.3461262719737096538, 4.658553426539353559, -3.671615880910378937 ) ) ;
#8024=VERTEX_POINT ( 'NONE', #10843 ) ;
#8051=CARTESIAN_POINT ( 'NONE',  ( -4.000000000000087041, 2.309401076758546445, -5.000000000000000888 ) ) ;
#8063=AXIS2_PLACEMENT_3D ( 'NONE', #11277, #18234, #5767 ) ;
#8111=CARTESIAN_POINT ( 'NONE',  ( 2.500000000000005329, -3.183331332160763538E-15, 1.084202172485504434E-16 ) ) ;
#8133=CARTESIAN_POINT ( 'NONE',  ( 0.000000000000000000, 0.000000000000000000, 3.469446951953614189E-15 ) ) ;
#8136=AXIS2_PLACEMENT_3D ( 'NONE', #8938, #19758, #3640 ) ;
#8138=CARTESIAN_POINT ( 'NONE',  ( -4.000000000000153655, -6.722053469410127491E-15, -3.142992957459292303 ) ) ;
#8195=CARTESIAN_POINT ( 'NONE',  ( -4.000000000000095923, 0.3987449864459913784, -0.01220643443066572048 ) ) ;
#8229=CARTESIAN_POINT ( 'NONE',  ( -2.000000000000020428, 3.464101615137764156, -3.142992957459267434 ) ) ;
#8251=CARTESIAN_POINT ( 'NONE',  ( 3.999999999999940936, 2.309401076758546445, -0.5000000000000004441 ) ) ;
#8258=ADVANCED_FACE ( 'NONE', ( #932 ), #8322, .T. ) ;
#8267=ORIENTED_EDGE ( 'NONE', *, *, #15622, .F. ) ;
#8286=DIRECTION ( 'NONE',  ( 1.333893503340774882E-15, 2.778352770573747380E-17, 1.000000000000000000 ) ) ;
#8298=EDGE_LOOP ( 'NONE', ( #4031, #1262, #19053, #4597, #7235, #15883, #12211 ) ) ;
#8302=CARTESIAN_POINT ( 'NONE',  ( 3.999999999999940936, 2.309401076758546445, -0.5000000000000004441 ) ) ;
#8322=PLANE ( 'NONE',  #19640 ) ;
#8353=CARTESIAN_POINT ( 'NONE',  ( -2.100000000000011635, 2.938364432290698513E-15, -5.000000000000003553 ) ) ;
#8375=ADVANCED_FACE ( 'NONE', ( #9222 ), #16379, .T. ) ;
#8381=ORIENTED_EDGE ( 'NONE', *, *, #21075, .F. ) ;
#8386=AXIS2_PLACEMENT_3D ( 'NONE', #3133, #23136, #10299 ) ;
#8395=AXIS2_PLACEMENT_3D ( 'NONE', #17906, #5443, #10836 ) ;
#8464=VERTEX_POINT ( 'NONE', #864 ) ;
#8481=CARTESIAN_POINT ( 'NONE',  ( 2.682243648011605863, 3.070208061305347957, -0.04852650426600601391 ) ) ;
#8501=CARTESIAN_POINT ( 'NONE',  ( 4.154306624731114006, 2.398490048084875426, -3.721999068284411738 ) ) ;
#8514=CARTESIAN_POINT ( 'NONE',  ( -4.000000000000103029, 2.471528634177575512, -3.686887442155210692 ) ) ;
#8543=AXIS2_PLACEMENT_3D ( 'NONE', #4208, #708, #22225 ) ;
#8558=CARTESIAN_POINT ( 'NONE',  ( -6.938893903907228378E-14, -4.618802153517121312, -5.000000000000011546 ) ) ;
#8581=ORIENTED_EDGE ( 'NONE', *, *, #14821, .F. ) ;
#8584=CARTESIAN_POINT ( 'NONE',  ( -0.1404048886733319235, -4.699864953788127409, -3.686887068327057371 ) ) ;
#8587=CARTESIAN_POINT ( 'NONE',  ( 0.000000000000000000, 0.000000000000000000, -4.974599999999998801 ) ) ;
#8621=CONICAL_SURFACE ( 'NONE', #14635, 2.500000000000015543, 0.9599310885968873608 ) ;
#8622=CARTESIAN_POINT ( 'NONE',  ( -3.679171394226111058, -2.494631558665882931, -0.3503314178413123314 ) ) ;
#8627=CARTESIAN_POINT ( 'NONE',  ( -4.000000000000108358, -2.512220745329347693, -3.469390707569752763 ) ) ;
#8656=FACE_OUTER_BOUND ( 'NONE', #22234, .T. ) ;
#8660=FILL_AREA_STYLE ('',( #3482 ) ) ;
#8680=CARTESIAN_POINT ( 'NONE',  ( -1.393927851585492039, 4.043713361053525190, -3.526374918436834704 ) ) ;
#8688=CARTESIAN_POINT ( 'NONE',  ( -3.436319922986721842, 2.634841920957935901, -3.531542292955571316 ) ) ;
#8748=EDGE_LOOP ( 'NONE', ( #10855, #17151 ) ) ;
#8766=CARTESIAN_POINT ( 'NONE',  ( -2.449848172108612943, -3.432307619358808903, -3.503702292528934503 ) ) ;
#8768=CARTESIAN_POINT ( 'NONE',  ( -4.197393957002394593, -7.172049766556752605E-14, -3.503767560748959120 ) ) ;
#8798=EDGE_CURVE ( 'NONE', #8024, #7652, #23044, .T. ) ;
#8805=EDGE_CURVE ( 'NONE', #19106, #13336, #20028, .T. ) ;
#8809=CARTESIAN_POINT ( 'NONE',  ( 0.1750025118120909495, 4.719839900820656631, -3.469254087858260505 ) ) ;
#8822=CARTESIAN_POINT ( 'NONE',  ( 4.175648173966012955, -2.207990556236570701, -3.469390959564061294 ) ) ;
#8823=FACE_OUTER_BOUND ( 'NONE', #1699, .T. ) ;
#8839=CARTESIAN_POINT ( 'NONE',  ( 3.999999999999939160, 0.1981133338132110011, 4.941929027460484850E-14 ) ) ;
#8846=ADVANCED_FACE ( 'NONE', ( #5202 ), #4250, .F. ) ;
#8847=ORIENTED_EDGE ( 'NONE', *, *, #13413, .F. ) ;
#8887=CARTESIAN_POINT ( 'NONE',  ( 0.02511973781845255188, -4.877415612947488377, -3.751298745799865664 ) ) ;
#8896=( NAMED_UNIT ( * ) PLANE_ANGLE_UNIT ( ) SI_UNIT ( $, .RADIAN. ) );
#8898=CARTESIAN_POINT ( 'NONE',  ( -4.197393957002394593, -7.172049766556752605E-14, -3.503767560748959120 ) ) ;
#8916=CIRCLE ( 'NONE', #17156, 2.500000000000014655 ) ;
#8925=DIRECTION ( 'NONE',  ( 1.333893503340774882E-15, 2.778352770573747380E-17, 1.000000000000000000 ) ) ;
#8938=CARTESIAN_POINT ( 'NONE',  ( 3.999999999999948042, 2.309401076758532678, -5.000000000000000888 ) ) ;
#8950=SURFACE_STYLE_FILL_AREA ( #12706 ) ;
#8954=CARTESIAN_POINT ( 'NONE',  ( -4.000000000000045297, 1.387778780781445676E-14, 0.000000000000000000 ) ) ;
#8994=ORIENTED_EDGE ( 'NONE', *, *, #19686, .T. ) ;
#9007=CARTESIAN_POINT ( 'NONE',  ( -4.235886605889470857, -2.417314728048573169, -3.751161874094045334 ) ) ;
#9009=FACE_OUTER_BOUND ( 'NONE', #18051, .T. ) ;
#9025=CYLINDRICAL_SURFACE ( 'NONE', #4595, 2.500000000000015543 ) ;
#9039=CARTESIAN_POINT ( 'NONE',  ( -0.6507732100474116210, 4.243078065514748864, -0.2236248678334617213 ) ) ;
#9065=B_SPLINE_CURVE_WITH_KNOTS ( 'NONE', 3,
 ( #15885, #4845, #19200, #6848 ),
 .UNSPECIFIED., .F., .F.,
 ( 4, 4 ),
 ( 0.000000000000000000, 0.002452478801916411870 ),
 .UNSPECIFIED. ) ;
#9070=CARTESIAN_POINT ( 'NONE',  ( -0.1756481739660878671, 4.720212674039040657, -3.469390959564085719 ) ) ;
#9074=( BOUNDED_SURFACE ( )  B_SPLINE_SURFACE ( 3, 2, ( 
 ( #11674, #6403, #7925 ),
 ( #6173, #15326, #18985 ),
 ( #9929, #13572, #2862 ),
 ( #13690, #19093, #15205 ),
 ( #17202, #9807, #1114 ),
 ( #4620, #4509, #647 ) ),
 .UNSPECIFIED., .F., .F., .T. ) 
 B_SPLINE_SURFACE_WITH_KNOTS ( ( 4, 2, 4 ),
 ( 3, 3 ),
 ( 0.02027065861071770947, 0.02273072267836921678, 0.02519078674602072410 ),
 ( 0.000000000000000000, 1.000000000000000000 ),
 .UNSPECIFIED. ) 
 GEOMETRIC_REPRESENTATION_ITEM ( )  RATIONAL_B_SPLINE_SURFACE ( (
 ( 1.000000000000000000, 0.8047781708337304885, 1.000000000000000000),
 ( 1.000000000000000000, 0.8123765190705294348, 1.000000000000000000),
 ( 1.000000000000000000, 0.8190656277163984589, 1.000000000000000000),
 ( 1.000000000000000000, 0.8192366903512168230, 1.000000000000000000),
 ( 1.000000000000000000, 0.8126138454302894720, 1.000000000000000000),
 ( 1.000000000000000000, 0.8047712246031424321, 1.000000000000000000) ) ) 
 REPRESENTATION_ITEM ( '' )  SURFACE ( )  );
#9129=ORIENTED_EDGE ( 'NONE', *, *, #22669, .F. ) ;
#9182=SURFACE_STYLE_USAGE ( .BOTH. , #1990 ) ;
#9183=CARTESIAN_POINT ( 'NONE',  ( 3.999999999999939160, 0.9868501483902684113, -0.09357334158575086880 ) ) ;
#9209=AXIS2_PLACEMENT_3D ( 'NONE', #15657, #16007, #5318 ) ;
#9217=ADVANCED_FACE ( 'NONE', ( #23181 ), #17951, .F. ) ;
#9222=FACE_OUTER_BOUND ( 'NONE', #10289, .T. ) ;
#9249=ORIENTED_EDGE ( 'NONE', *, *, #4183, .F. ) ;
#9262=( BOUNDED_SURFACE ( )  B_SPLINE_SURFACE ( 3, 2, ( 
 ( #21712, #10758, #9007 ),
 ( #12760, #16278, #16159 ),
 ( #14642, #18066, #77 ),
 ( #7140, #7247, #19823 ),
 ( #19945, #12637, #21603 ),
 ( #11103, #5249, #8887 ) ),
 .UNSPECIFIED., .F., .F., .F. ) 
 B_SPLINE_SURFACE_WITH_KNOTS ( ( 4, 2, 4 ),
 ( 3, 3 ),
 ( 0.02032853247518129000, 0.02278863295364823988, 0.02524873343211518975 ),
 ( 0.000000000000000000, 1.000000000000000000 ),
 .UNSPECIFIED. ) 
 GEOMETRIC_REPRESENTATION_ITEM ( )  RATIONAL_B_SPLINE_SURFACE ( (
 ( 1.000000000000000000, 0.8047781615896834051, 1.000000000000000000),
 ( 1.000000000000000000, 0.8123767586289972753, 1.000000000000000000),
 ( 1.000000000000000000, 0.8190662415563431109, 1.000000000000000000),
 ( 1.000000000000000000, 0.8192361015669969992, 1.000000000000000000),
 ( 1.000000000000000000, 0.8126135807103180841, 1.000000000000000000),
 ( 1.000000000000000000, 0.8047712338318581127, 1.000000000000000000) ) ) 
 REPRESENTATION_ITEM ( '' )  SURFACE ( )  );
#9324=VECTOR ( 'NONE', #4591, 1000.000000000000000 ) ;
#9353=COLOUR_RGB ( '', 0.31764706, 0.68627451, 0.89019608) ;
#9359=CONICAL_SURFACE ( 'NONE', #22511, 4.000000000000022204, 0.8911886515913840512 ) ;
#9376=CARTESIAN_POINT ( 'NONE',  ( -0.6448876103709475505, -4.246476118072399331, -0.2256878752777136121 ) ) ;
#9395=CARTESIAN_POINT ( 'NONE',  ( -4.000000000000087041, 2.309401076758546445, -5.000000000000000888 ) ) ;
#9445=VECTOR ( 'NONE', #7672, 1000.000000000000000 ) ;
#9480=CARTESIAN_POINT ( 'NONE',  ( 6.938893903907228378E-15, 4.618802153517023612, -3.433295621305385126 ) ) ;
#9484=CARTESIAN_POINT ( 'NONE',  ( -4.211140560182305315, -2.431303136016589761, -3.745885042887437510 ) ) ;
#9489=DIRECTION ( 'NONE',  ( 1.333893503340774882E-15, 2.778352770573747380E-17, 1.000000000000000000 ) ) ;
#9500=EDGE_CURVE ( 'NONE', #9648, #2950, #15497, .T. ) ;
#9553=CARTESIAN_POINT ( 'NONE',  ( 4.197393957002246268, 0.8151795401431507493, -3.503767560748920040 ) ) ;
#9560=VERTEX_POINT ( 'NONE', #15490 ) ;
#9582=CARTESIAN_POINT ( 'NONE',  ( -4.211140560182305315, -2.431303136016589761, -3.745885042887437510 ) ) ;
#9648=VERTEX_POINT ( 'NONE', #12188 ) ;
#9675=VECTOR ( 'NONE', #18290, 1000.000000000000000 ) ;
#9707=VERTEX_POINT ( 'NONE', #9480 ) ;
#9719=CARTESIAN_POINT ( 'NONE',  ( 0.000000000000000000, 0.000000000000000000, -0.2800830152838822418 ) ) ;
#9728=ADVANCED_FACE ( 'NONE', ( #18536 ), #9025, .F. ) ;
#9754=CARTESIAN_POINT ( 'NONE',  ( -4.154094228333751637, -2.398367420967737917, -3.721909803043223164 ) ) ;
#9783=CARTESIAN_POINT ( 'NONE',  ( -4.000000000000098588, 1.539600717839030741, -3.300726591567078483 ) ) ;
#9807=CARTESIAN_POINT ( 'NONE',  ( 3.999999999998528288, 1.658577278524556942, -3.531553309553837838 ) ) ;
#9821=EDGE_CURVE ( 'NONE', #13336, #19106, #16610, .T. ) ;
#9866=DIRECTION ( 'NONE',  ( -1.000000000000000000, 1.276756478318923119E-15, -1.333893503340766797E-15 ) ) ;
#9878=CARTESIAN_POINT ( 'NONE',  ( -2.345747346278134859, 3.264484291692478113, -0.01223254789873211984 ) ) ;
#9906=DIRECTION ( 'NONE',  ( 1.000000000000000000, -1.276756478318922922E-15, 1.333893503340766994E-15 ) ) ;
#9929=CARTESIAN_POINT ( 'NONE',  ( 3.999999999999976463, -0.8732470631450403031, -3.223155494240571795 ) ) ;
#9959=CARTESIAN_POINT ( 'NONE',  ( 3.333333333333291737, 2.694301256218282870, -3.300726591567082924 ) ) ;
#10012=CARTESIAN_POINT ( 'NONE',  ( -0.6937372685066998113, 4.453844082567709250, -3.610536846335886008 ) ) ;
#10066=DIRECTION ( 'NONE',  ( 1.000000000000000000, -1.276756478318923119E-15, 1.387778780781436998E-15 ) ) ;
#10088=EDGE_LOOP ( 'NONE', ( #6166, #8381, #11720 ) ) ;
#10131=EDGE_CURVE ( 'NONE', #11666, #2382, #17814, .T. ) ;
#10150=CARTESIAN_POINT ( 'NONE',  ( 4.211140560182139225, 2.431303136016540911, -3.745885042887430405 ) ) ;
#10156=CARTESIAN_POINT ( 'NONE',  ( -4.000000000000087041, -2.309401076758553550, -0.5000000000000004441 ) ) ;
#10236=EDGE_CURVE ( 'NONE', #10905, #22731, #4877, .T. ) ;
#10272=CARTESIAN_POINT ( 'NONE',  ( -4.000000000000104805, 0.8730739991738779571, -3.223134629628646941 ) ) ;
#10285=EDGE_LOOP ( 'NONE', ( #15218, #18616, #13926, #14992, #7350 ) ) ;
#10289=EDGE_LOOP ( 'NONE', ( #16723, #10698, #21862, #19729, #6183 ) ) ;
#10299=DIRECTION ( 'NONE',  ( -1.000000000000000000, 1.276756478318923119E-15, -1.403805528459192781E-15 ) ) ;
#10315=EDGE_CURVE ( 'NONE', #19106, #6591, #5931, .T. ) ;
#10333=CARTESIAN_POINT ( 'NONE',  ( -2.855764796983377263, 2.970025579236395874, -0.09382832055445512742 ) ) ;
#10366=ORIENTED_EDGE ( 'NONE', *, *, #23149, .F. ) ;
#10373=CARTESIAN_POINT ( 'NONE',  ( 1.999999999999953149, -3.464101615137771262, 0.000000000000000000 ) ) ;
#10389=CARTESIAN_POINT ( 'NONE',  ( -4.211399284164375700, 2.459729995988197526, -3.751162237960563139 ) ) ;
#10412=CARTESIAN_POINT ( 'NONE',  ( -2.804994570502229223, -3.229033611042515073, -3.526374918436863126 ) ) ;
#10468=CARTESIAN_POINT ( 'NONE',  ( 2.855764796983322640, -2.970025579236485136, -0.09382832055448196706 ) ) ;
#10484=VERTEX_POINT ( 'NONE', #15981 ) ;
#10502=CARTESIAN_POINT ( 'NONE',  ( 1.391697335622787080, 4.043246145443402995, -3.503898532754375239 ) ) ;
#10553=EDGE_CURVE ( 'NONE', #11666, #15881, #22103, .T. ) ;
#10558=CARTESIAN_POINT ( 'NONE',  ( -2.805705207896105779, 3.226868319750133107, -3.503898532754362805 ) ) ;
#10573=CARTESIAN_POINT ( 'NONE',  ( 3.436319922986410536, -2.634841920959276163, -3.531542292954277240 ) ) ;
#10577=CARTESIAN_POINT ( 'NONE',  ( 6.938893903907228378E-15, 4.618802153517023612, -3.433295621305385126 ) ) ;
#10587=CARTESIAN_POINT ( 'NONE',  ( 3.999999999999950706, 1.539600717839022082, -3.300726591567077595 ) ) ;
#10618=CARTESIAN_POINT ( 'NONE',  ( -4.000000000000108358, -2.472261339043379635, -3.687027428081224301 ) ) ;
#10698=ORIENTED_EDGE ( 'NONE', *, *, #368, .T. ) ;
#10705=CARTESIAN_POINT ( 'NONE',  ( 2.100000000000011635, -2.681188604469753282E-15, -0.2800830152838794107 ) ) ;
#10714=ORIENTED_EDGE ( 'NONE', *, *, #20170, .T. ) ;
#10719=CARTESIAN_POINT ( 'NONE',  ( 4.140404888673258732, 2.228338276487474179, -3.686887068327037831 ) ) ;
#10730=DIRECTION ( 'NONE',  ( 1.000000000000000000, -1.276756478318922330E-15, 0.000000000000000000 ) ) ;
#10741=ORIENTED_EDGE ( 'NONE', *, *, #2682, .T. ) ;
#10750=ORIENTED_EDGE ( 'NONE', *, *, #14821, .T. ) ;
#10758=CARTESIAN_POINT ( 'NONE',  ( -4.140404888673358208, -2.228338276487483505, -3.686887068327060035 ) ) ;
#10806=CARTESIAN_POINT ( 'NONE',  ( 0.5276280594149747039, -4.314175951381801433, -3.320322319201818750 ) ) ;
#10813=EDGE_CURVE ( 'NONE', #405, #7652, #7598, .T. ) ;
#10836=DIRECTION ( 'NONE',  ( 1.000000000000000000, -1.276756478318923119E-15, 1.403805528459192781E-15 ) ) ;
#10843=CARTESIAN_POINT ( 'NONE',  ( 5.560781378645629047, -7.086303797513785838E-15, -4.000000000000000000 ) ) ;
#10855=ORIENTED_EDGE ( 'NONE', *, *, #19686, .F. ) ;
#10899=B_SPLINE_CURVE_WITH_KNOTS ( 'NONE', 3,
 ( #13602, #9959, #12045, #2655, #6313 ),
 .UNSPECIFIED., .F., .F.,
 ( 4, 1, 4 ),
 ( 0.000000000000000000, 0.002309401076758509259, 0.004618802153517017652 ),
 .UNSPECIFIED. ) ;
#10905=VERTEX_POINT ( 'NONE', #19739 ) ;
#10948=DIRECTION ( 'NONE',  ( -1.276756478318923119E-15, -1.000000000000000000, 2.778352770573917478E-17 ) ) ;
#10990=EDGE_CURVE ( 'NONE', #22002, #2089, #11585, .T. ) ;
#11003=VERTEX_POINT ( 'NONE', #9484 ) ;
#11042=CARTESIAN_POINT ( 'NONE',  ( -4.101948962586008385, -2.368261337751097706, -3.681124513963646372 ) ) ;
#11047=CARTESIAN_POINT ( 'NONE',  ( -4.000000000000096811, -0.3979232138631050297, -6.754240721405789642E-14 ) ) ;
#11103=CARTESIAN_POINT ( 'NONE',  ( 0.1756481739660004926, -4.720212674039055756, -3.469390959564091492 ) ) ;
#11106=CARTESIAN_POINT ( 'NONE',  ( 2.500000000000015543, 1.068589661201712855E-14, -25.03750572909315153 ) ) ;
#11168=DIRECTION ( 'NONE',  ( 1.333893503340774882E-15, 2.778352770573747380E-17, 1.000000000000000000 ) ) ;
#11184=B_SPLINE_CURVE_WITH_KNOTS ( 'NONE', 3,
 ( #18489, #1903, #18264, #12851, #14848, #21578 ),
 .UNSPECIFIED., .F., .F.,
 ( 4, 2, 4 ),
 ( 0.003358874760055623448, 0.004541967308452153629, 0.005725059856848683376 ),
 .UNSPECIFIED. ) ;
#11222=FACE_OUTER_BOUND ( 'NONE', #4524, .T. ) ;
#11274=CARTESIAN_POINT ( 'NONE',  ( -4.211140560182305315, -2.431303136016589761, -3.745885042887437510 ) ) ;
#11277=CARTESIAN_POINT ( 'NONE',  ( 0.000000000000000000, 0.000000000000000000, -0.2800830152838822418 ) ) ;
#11322=DIRECTION ( 'NONE',  ( -1.000000000000000000, 1.276756478318922725E-15, -1.333893503340766402E-15 ) ) ;
#11360=EDGE_CURVE ( 'NONE', #14190, #11003, #21689, .T. ) ;
#11371=DIRECTION ( 'NONE',  ( 1.000000000000000000, -1.276756478318923119E-15, 1.403805528459192781E-15 ) ) ;
#11382=AXIS2_PLACEMENT_3D ( 'NONE', #18027, #5084, #15773 ) ;
#11414=CARTESIAN_POINT ( 'NONE',  ( -2.500000000000015543, 1.737584070339862599E-14, -25.03750572909315864 ) ) ;
#11452=CARTESIAN_POINT ( 'NONE',  ( 6.938893903907228378E-15, 4.618802153517023612, -5.000000000000000888 ) ) ;
#11455=LINE ( 'NONE', #20410, #2879 ) ;
#11464=VERTEX_POINT ( 'NONE', #13458 ) ;
#11496=AXIS2_PLACEMENT_3D ( 'NONE', #18337, #6101, #5873 ) ;
#11504=CYLINDRICAL_SURFACE ( 'NONE', #8543, 2.100000000000011635 ) ;
#11517=ADVANCED_FACE ( 'NONE', ( #6515 ), #9074, .F. ) ;
#11528=CARTESIAN_POINT ( 'NONE',  ( -4.211140560182312420, 2.431303136016568889, -3.745885042887433958 ) ) ;
#11535=COLOUR_RGB ( '', 0.31764706, 0.68627451, 0.89019608) ;
#11559=CARTESIAN_POINT ( 'NONE',  ( 4.024499207728609029, 2.323545700935586655, -3.572172305156459338 ) ) ;
#11585=B_SPLINE_CURVE_WITH_KNOTS ( 'NONE', 3,
 ( #5734, #21734, #9376, #3722, #5620, #12901, #4176, #16523 ),
 .UNSPECIFIED., .F., .F.,
 ( 4, 2, 2, 4 ),
 ( 2.465131517636197337E-07, 0.001183067374689898569, 0.001774477805458966450, 0.002365888236228034115 ),
 .UNSPECIFIED. ) ;
#11587=EDGE_LOOP ( 'NONE', ( #3920, #20508, #20622, #9249 ) ) ;
#11627=CARTESIAN_POINT ( 'NONE',  ( 6.938893903907228378E-15, 4.618802153517023612, -3.433295621305385126 ) ) ;
#11648=FACE_OUTER_BOUND ( 'NONE', #10088, .T. ) ;
#11653=ADVANCED_FACE ( 'NONE', ( #23222 ), #18528, .F. ) ;
#11666=VERTEX_POINT ( 'NONE', #6991 ) ;
#11674=CARTESIAN_POINT ( 'NONE',  ( 3.999999999999975131, -2.511475576507315566, -3.469253905236648006 ) ) ;
#11681=CIRCLE ( 'NONE', #21485, 4.000000000000023093 ) ;
#11720=ORIENTED_EDGE ( 'NONE', *, *, #22317, .F. ) ;
#11723=ORIENTED_EDGE ( 'NONE', *, *, #8805, .T. ) ;
#11744=CARTESIAN_POINT ( 'NONE',  ( -3.333333333333423631, 2.694301256218305518, -3.300726591567079371 ) ) ;
#11801=EDGE_CURVE ( 'NONE', #22849, #8024, #3141, .T. ) ;
#11815=EDGE_CURVE ( 'NONE', #11464, #19280, #16265, .T. ) ;
#11827=FACE_OUTER_BOUND ( 'NONE', #22788, .T. ) ;
#11874=AXIS2_PLACEMENT_3D ( 'NONE', #577, #2218, #5642 ) ;
#11884=CARTESIAN_POINT ( 'NONE',  ( 3.349226789952567618, 2.685125164760785221, -0.2236248678334500084 ) ) ;
#11932=TOROIDAL_SURFACE ( 'NONE', #2166, 5.384454397937119552, 0.5155456020628805813 ) ;
#11933=CARTESIAN_POINT ( 'NONE',  ( -6.245004513516505540E-14, -4.862606272033144883, -3.745885042887461935 ) ) ;
#11977=DIRECTION ( 'NONE',  ( 1.333893503340774882E-15, 2.778352770573747380E-17, 1.000000000000000000 ) ) ;
#12038=ORIENTED_EDGE ( 'NONE', *, *, #3128, .T. ) ;
#12045=CARTESIAN_POINT ( 'NONE',  ( 1.999999999999992673, 3.464101615137806789, -3.142992957459250114 ) ) ;
#12111=CARTESIAN_POINT ( 'NONE',  ( 2.100000000000011635, -2.681188604469753282E-15, -4.999999999999998224 ) ) ;
#12171=CARTESIAN_POINT ( 'NONE',  ( -2.500000000000015543, 3.191891195797327420E-15, -4.974600000000002353 ) ) ;
#12174=DIRECTION ( 'NONE',  ( -0.8660254037844358210, 0.5000000000000046629, -1.141293895983254122E-15 ) ) ;
#12188=CARTESIAN_POINT ( 'NONE',  ( 2.500000000000002220, 1.124296205839700427E-14, -5.000000000000004441 ) ) ;
#12211=ORIENTED_EDGE ( 'NONE', *, *, #15622, .T. ) ;
#12212=CARTESIAN_POINT ( 'NONE',  ( 3.680118525130219531, -2.494084732383396119, -0.3507732604232581819 ) ) ;
#12226=ORIENTED_EDGE ( 'NONE', *, *, #17678, .F. ) ;
#12237=CARTESIAN_POINT ( 'NONE',  ( 4.175002511812132333, 2.208363329454923640, -3.469254087858248514 ) ) ;
#12288=B_SPLINE_CURVE_WITH_KNOTS ( 'NONE', 3,
 ( #14243, #17768, #1988, #6833, #3754, #14475 ),
 .UNSPECIFIED., .F., .F.,
 ( 4, 2, 4 ),
 ( 0.000000000000000000, 0.0002095117440854730128, 0.0004190234881709460255 ),
 .UNSPECIFIED. ) ;
#12344=CARTESIAN_POINT ( 'NONE',  ( -4.000000000000087041, -2.309401076758553550, -0.5000000000000004441 ) ) ;
#12374=DIRECTION ( 'NONE',  ( 1.333893503340774882E-15, 2.778352770573747380E-17, 1.000000000000000000 ) ) ;
#12381=CARTESIAN_POINT ( 'NONE',  ( -4.204114297095823183, 1.660363174096529892, -3.602136431857980270 ) ) ;
#12413=SURFACE_SIDE_STYLE ('',( #19596 ) ) ;
#12421=ORIENTED_EDGE ( 'NONE', *, *, #10813, .F. ) ;
#12433=CARTESIAN_POINT ( 'NONE',  ( -3.511755186886851288, 2.826662030176404716, -3.597382984111576754 ) ) ;
#12457=DIRECTION ( 'NONE',  ( -1.000000000000000000, 1.276756478318923119E-15, -1.387778780781436998E-15 ) ) ;
#12471=EDGE_LOOP ( 'NONE', ( #9129, #2445, #20415 ) ) ;
#12472=ORIENTED_EDGE ( 'NONE', *, *, #19933, .F. ) ;
#12475=CARTESIAN_POINT ( 'NONE',  ( 2.742827927723032300, 3.035229711105330352, -3.433252694550416706 ) ) ;
#12488=AXIS2_PLACEMENT_3D ( 'NONE', #12777, #2299, #19960 ) ;
#12499=ORIENTED_EDGE ( 'NONE', *, *, #1356, .T. ) ;
#12536=EDGE_LOOP ( 'NONE', ( #1666, #14399, #6266, #8581, #12626, #17333 ) ) ;
#12539=EDGE_CURVE ( 'NONE', #18554, #6591, #3912, .T. ) ;
#12600=CARTESIAN_POINT ( 'NONE',  ( 0.5449313310646434205, 4.304185902837014410, -3.316620875263985191 ) ) ;
#12626=ORIENTED_EDGE ( 'NONE', *, *, #22669, .T. ) ;
#12637=CARTESIAN_POINT ( 'NONE',  ( -0.5636800770137567751, -4.293361309318373564, -3.531542292954506390 ) ) ;
#12645=B_SPLINE_CURVE_WITH_KNOTS ( 'NONE', 3,
 ( #4329, #2232, #21999, #16453, #18689, #13291, #13175, #364 ),
 .UNSPECIFIED., .F., .F.,
 ( 4, 2, 2, 4 ),
 ( 2.465131517408427001E-07, 0.001183067374689895750, 0.001774477805458973606, 0.002365888236228051462 ),
 .UNSPECIFIED. ) ;
#12706=FILL_AREA_STYLE ('',( #5187 ) ) ;
#12719=CARTESIAN_POINT ( 'NONE',  ( 1.390230914382568406, 4.043987460488565944, -3.502507215260532547 ) ) ;
#12727=AXIS2_PLACEMENT_3D ( 'NONE', #5403, #8925, #19512 ) ;
#12760=CARTESIAN_POINT ( 'NONE',  ( -3.472371940586150618, -2.614027278893177542, -3.320322319201808980 ) ) ;
#12770=ORIENTED_EDGE ( 'NONE', *, *, #23149, .T. ) ;
#12777=CARTESIAN_POINT ( 'NONE',  ( 0.000000000000000000, 0.000000000000000000, -4.694516984716116781 ) ) ;
#12798=CARTESIAN_POINT ( 'NONE',  ( 0.000000000000000000, 0.000000000000000000, -4.000000000000000000 ) ) ;
#12812=CARTESIAN_POINT ( 'NONE',  ( -4.000000000000045297, 1.387778780781445676E-14, 0.000000000000000000 ) ) ;
#12819=CARTESIAN_POINT ( 'NONE',  ( 3.999999999999940048, 1.941961291383530019, -0.3515519931179958424 ) ) ;
#12851=CARTESIAN_POINT ( 'NONE',  ( 3.999999999999936939, -0.7890432684751291781, -0.04868663549878041868 ) ) ;
#12901=CARTESIAN_POINT ( 'NONE',  ( -1.654252653722019684, -3.663718938583052420, -0.01223254789879538000 ) ) ;
#12927=CARTESIAN_POINT ( 'NONE',  ( -2.869520281200714380E-14, 4.647089433458816643, -3.572167766733388206 ) ) ;
#12934=CIRCLE ( 'NONE', #17442, 5.384454397937147974 ) ;
#12946=ORIENTED_EDGE ( 'NONE', *, *, #2017, .T. ) ;
#12981=ORIENTED_EDGE ( 'NONE', *, *, #8805, .F. ) ;
#13100=TOROIDAL_SURFACE ( 'NONE', #12727, 5.384454397937119552, 0.5155456020628805813 ) ;
#13108=B_SPLINE_CURVE_WITH_KNOTS ( 'NONE', 3,
 ( #4483, #9783, #8138, #737, #4356 ),
 .UNSPECIFIED., .F., .F.,
 ( 4, 1, 4 ),
 ( 0.000000000000000000, 0.002309401076758508826, 0.004618802153517017652 ),
 .UNSPECIFIED. ) ;
#13112=B_SPLINE_CURVE_WITH_KNOTS ( 'NONE', 3,
 ( #965, #15408, #8481, #11884, #2954, #8251 ),
 .UNSPECIFIED., .F., .F.,
 ( 4, 2, 4 ),
 ( 0.002365888236228051462, 0.003551327329835092354, 0.004736766423442132813 ),
 .UNSPECIFIED. ) ;
#13119=ADVANCED_FACE ( 'NONE', ( #22009 ), #6247, .T. ) ;
#13173=CARTESIAN_POINT ( 'NONE',  ( 0.000000000000000000, 0.000000000000000000, -0.3080913168122673129 ) ) ;
#13175=CARTESIAN_POINT ( 'NONE',  ( 1.828356344711600467, 3.563200125723214651, -8.699875401248920360E-15 ) ) ;
#13178=( BOUNDED_SURFACE ( )  B_SPLINE_SURFACE ( 3, 2, ( 
 ( #5226, #8514, #10389 ),
 ( #19445, #19214, #12381 ),
 ( #10272, #15567, #22870 ),
 ( #19563, #17808, #15788 ),
 ( #17923, #3348, #3452 ),
 ( #8627, #10618, #7116 ) ),
 .UNSPECIFIED., .F., .F., .T. ) 
 B_SPLINE_SURFACE_WITH_KNOTS ( ( 4, 2, 4 ),
 ( 3, 3 ),
 ( 0.02027752710269158445, 0.02273781595091097646, 0.02519810479913037193 ),
 ( 0.000000000000000000, 1.000000000000000000 ),
 .UNSPECIFIED. ) 
 GEOMETRIC_REPRESENTATION_ITEM ( )  RATIONAL_B_SPLINE_SURFACE ( (
 ( 1.000000000000000000, 0.8047781431712803801, 1.000000000000000000),
 ( 1.000000000000000000, 0.8123773247083573290, 1.000000000000000000),
 ( 1.000000000000000000, 0.8190670192155369289, 1.000000000000000000),
 ( 1.000000000000000000, 0.8192353552911690873, 1.000000000000000000),
 ( 1.000000000000000000, 0.8126132098227178968, 1.000000000000000000),
 ( 1.000000000000000000, 0.8047712465856385888, 1.000000000000000000) ) ) 
 REPRESENTATION_ITEM ( '' )  SURFACE ( )  );
#13232=ORIENTED_EDGE ( 'NONE', *, *, #17001, .F. ) ;
#13258=AXIS2_PLACEMENT_3D ( 'NONE', #8558, #16264, #18057 ) ;
#13283=CARTESIAN_POINT ( 'NONE',  ( -2.000000000000119904, -3.464101615137792134, -1.040834085586084257E-14 ) ) ;
#13291=CARTESIAN_POINT ( 'NONE',  ( 1.654252653721867139, 3.663718938583046647, -0.01223254789874405647 ) ) ;
#13298=ADVANCED_FACE ( 'NONE', ( #1411 ), #8621, .F. ) ;
#13318=CARTESIAN_POINT ( 'NONE',  ( -2.500000000000023981, 3.506612759220730751E-15, 6.830473686658677934E-15 ) ) ;
#13336=VERTEX_POINT ( 'NONE', #1864 ) ;
#13393=CARTESIAN_POINT ( 'NONE',  ( 0.000000000000000000, 0.000000000000000000, 0.000000000000000000 ) ) ;
#13409=AXIS2_PLACEMENT_3D ( 'NONE', #8051, #4277, #18637 ) ;
#13410=MECHANICAL_DESIGN_GEOMETRIC_PRESENTATION_REPRESENTATION('',(#13799),#6664);
#13413=EDGE_CURVE ( 'NONE', #6303, #9707, #6463, .T. ) ;
#13419=ADVANCED_FACE ( 'NONE', ( #3008 ), #14270, .T. ) ;
#13427=CARTESIAN_POINT ( 'NONE',  ( -6.958621627098453431E-14, -4.618802153517120423, -3.504271511726807731 ) ) ;
#13458=CARTESIAN_POINT ( 'NONE',  ( -2.500000000000006217, 3.191891195797315193E-15, -4.974599999999995248 ) ) ;
#13467=VERTEX_POINT ( 'NONE', #8302 ) ;
#13493=CIRCLE ( 'NONE', #2978, 5.384454397937147974 ) ;
#13496=ORIENTED_EDGE ( 'NONE', *, *, #11360, .F. ) ;
#13542=DIRECTION ( 'NONE',  ( -1.000000000000000000, 1.276756478318923119E-15, -1.333893503340766797E-15 ) ) ;
#13572=CARTESIAN_POINT ( 'NONE',  ( 3.999999999999606537, -0.8578082829538927756, -3.433262215449805144 ) ) ;
#13602=CARTESIAN_POINT ( 'NONE',  ( 3.999999999999948042, 2.309401076758532678, -3.433295621305378020 ) ) ;
#13629=AXIS2_PLACEMENT_3D ( 'NONE', #7354, #21481, #16273 ) ;
#13640=CARTESIAN_POINT ( 'NONE',  ( -3.355112389629213876, 2.681727112203128538, -0.2256878752776726449 ) ) ;
#13642=CONICAL_SURFACE ( 'NONE', #8386, 5.560781378645605066, 1.221730476396047704 ) ;
#13662=B_SPLINE_CURVE_WITH_KNOTS ( 'NONE', 3,
 ( #16339, #18009, #5184, #10587, #23192 ),
 .UNSPECIFIED., .F., .F.,
 ( 4, 1, 4 ),
 ( 0.000000000000000000, 0.002309401076758509259, 0.004618802153517018519 ),
 .UNSPECIFIED. ) ;
#13673=EDGE_LOOP ( 'NONE', ( #7318, #22706, #19271 ) ) ;
#13676=AXIS2_PLACEMENT_3D ( 'NONE', #17837, #1483, #3139 ) ;
#13678=ORIENTED_EDGE ( 'NONE', *, *, #19207, .T. ) ;
#13690=CARTESIAN_POINT ( 'NONE',  ( 3.999999999999978240, 0.8378280264232709218, -3.220590601395822983 ) ) ;
#13746=CARTESIAN_POINT ( 'NONE',  ( -5.384454397937147974, 7.534042519137932791E-15, -4.484454397937126302 ) ) ;
#13765=ADVANCED_FACE ( 'NONE', ( #11222 ), #19536, .T. ) ;
#13787=UNCERTAINTY_MEASURE_WITH_UNIT (LENGTH_MEASURE( 1.000000000000000082E-05 ), #7026, 'distance_accuracy_value', 'NONE');
#13799=STYLED_ITEM ( 'NONE', ( #16102 ), #21055 ) ;
#13800=CARTESIAN_POINT ( 'NONE',  ( 0.000000000000000000, 0.000000000000000000, -0.3080913168122673129 ) ) ;
#13814=CIRCLE ( 'NONE', #15662, 4.000000000000022204 ) ;
#13898=EDGE_LOOP ( 'NONE', ( #2147, #4980, #18725 ) ) ;
#13909=LINE ( 'NONE', #4848, #7040 ) ;
#13926=ORIENTED_EDGE ( 'NONE', *, *, #3761, .T. ) ;
#13933=CARTESIAN_POINT ( 'NONE',  ( 0.3461262719735577198, -4.658553426539340236, -3.671615880910400254 ) ) ;
#14047=ORIENTED_EDGE ( 'NONE', *, *, #2682, .F. ) ;
#14076=ORIENTED_EDGE ( 'NONE', *, *, #10813, .T. ) ;
#14097=CARTESIAN_POINT ( 'NONE',  ( -1.257172072276703467, 3.892973519170507934, -3.433252694550608553 ) ) ;
#14100=CARTESIAN_POINT ( 'NONE',  ( -1.655952806101454788, 3.662737355149022545, 2.873135757086587539E-15 ) ) ;
#14151=CARTESIAN_POINT ( 'NONE',  ( 2.449848172108562316, 3.432307619358748951, -3.503702292528913187 ) ) ;
#14190=VERTEX_POINT ( 'NONE', #5558 ) ;
#14198=AXIS2_PLACEMENT_3D ( 'NONE', #21605, #5481, #12174 ) ;
#14221=CARTESIAN_POINT ( 'NONE',  ( -3.455068668935409093, 2.624017327438563640, -3.316620875264115753 ) ) ;
#14222=CARTESIAN_POINT ( 'NONE',  ( -2.000000000000036415, 3.464101615137757495, 0.000000000000000000 ) ) ;
#14231=CARTESIAN_POINT ( 'NONE',  ( 2.725741868436434068, -3.045094352033816953, -3.220599429844055894 ) ) ;
#14243=CARTESIAN_POINT ( 'NONE',  ( 3.999999999999955147, -2.309401076758532678, -3.433295621305388678 ) ) ;
#14258=CARTESIAN_POINT ( 'NONE',  ( 4.235886605889370493, 2.417314728048562067, -3.751161874094022686 ) ) ;
#14270=CONICAL_SURFACE ( 'NONE', #4107, 4.000000000000022204, 0.8911886515913840512 ) ;
#14299=CARTESIAN_POINT ( 'NONE',  ( -4.154094228334058947, 2.398367420967200569, -3.721909803043219611 ) ) ;
#14313=ORIENTED_EDGE ( 'NONE', *, *, #18177, .F. ) ;
#14326=CARTESIAN_POINT ( 'NONE',  ( -4.175648173966148846, 2.207990556236534729, -3.469390959564085719 ) ) ;
#14327=EDGE_CURVE ( 'NONE', #2950, #11464, #22592, .T. ) ;
#14329=CARTESIAN_POINT ( 'NONE',  ( -0.3208286057740161734, 4.433571671609661813, -0.3503314178412331725 ) ) ;
#14399=ORIENTED_EDGE ( 'NONE', *, *, #19207, .F. ) ;
#14407=EDGE_CURVE ( 'NONE', #22641, #7652, #4344, .T. ) ;
#14416=PLANE ( 'NONE',  #14198 ) ;
#14437=CARTESIAN_POINT ( 'NONE',  ( 0.000000000000000000, 1.387778780781445676E-14, -25.03750572909315508 ) ) ;
#14463=CARTESIAN_POINT ( 'NONE',  ( 3.455068668934203391, -2.624017327439216896, -3.316620875263055712 ) ) ;
#14464=CARTESIAN_POINT ( 'NONE',  ( 2.687328764639619116, -3.067272167851354592, -0.05923475698273424767 ) ) ;
#14475=CARTESIAN_POINT ( 'NONE',  ( 4.211140560182194292, -2.431303136016568889, -3.745885042887441063 ) ) ;
#14522=CARTESIAN_POINT ( 'NONE',  ( -4.197393957002393705, 0.4069871074557405710, -3.503767560748956011 ) ) ;
#14524=DIRECTION ( 'NONE',  ( 1.333893503340774882E-15, 2.778352770573747380E-17, 1.000000000000000000 ) ) ;
#14635=AXIS2_PLACEMENT_3D ( 'NONE', #8587, #22952, #21186 ) ;
#14636=CARTESIAN_POINT ( 'NONE',  ( 4.198928548860714649, -0.8158838809860312624, -3.526471437616904403 ) ) ;
#14642=CARTESIAN_POINT ( 'NONE',  ( -2.756197834950217640, -3.027510591568727705, -3.223146290109647261 ) ) ;
#14673=VECTOR ( 'NONE', #962, 1000.000000000000000 ) ;
#14727=AXIS2_PLACEMENT_3D ( 'NONE', #13746, #20928, #4794 ) ;
#14744=CARTESIAN_POINT ( 'NONE',  ( 4.204015924366130363, -1.626724848190950867, -3.610627190413379317 ) ) ;
#14821=EDGE_CURVE ( 'NONE', #22298, #15772, #11681, .T. ) ;
#14848=CARTESIAN_POINT ( 'NONE',  ( 3.999999999999937828, -0.3979232138631629834, 4.499947235583196612E-14 ) ) ;
#14856=ORIENTED_EDGE ( 'NONE', *, *, #4653, .T. ) ;
#14876=DIRECTION ( 'NONE',  ( 1.333893503340766797E-15, -2.778352770574087576E-17, -1.000000000000000000 ) ) ;
#14881=DIRECTION ( 'NONE',  ( -1.333893503340774882E-15, -2.778352770573747380E-17, -1.000000000000000000 ) ) ;
#14946=VECTOR ( 'NONE', #15211, 1000.000000000000000 ) ;
#14992=ORIENTED_EDGE ( 'NONE', *, *, #10990, .T. ) ;
#14998=ORIENTED_EDGE ( 'NONE', *, *, #18013, .T. ) ;
#15017=ORIENTED_EDGE ( 'NONE', *, *, #19933, .T. ) ;
#15018=ORIENTED_EDGE ( 'NONE', *, *, #12539, .T. ) ;
#15046=CARTESIAN_POINT ( 'NONE',  ( -0.02511973781853877458, 4.877415612947472390, -3.751298745799859891 ) ) ;
#15123=AXIS2_PLACEMENT_3D ( 'NONE', #19012, #2886, #10066 ) ;
#15146=AXIS2_PLACEMENT_3D ( 'NONE', #1898, #19913, #7553 ) ;
#15205=CARTESIAN_POINT ( 'NONE',  ( 4.197310751797331818, 0.8178363989515984311, -3.502498386812460840 ) ) ;
#15211=DIRECTION ( 'NONE',  ( 0.8191520442889933529, -1.029921702463443268E-15, 0.5735764363510438280 ) ) ;
#15212=DIRECTION ( 'NONE',  ( -0.8191520442889939080, 1.162110848990233300E-15, 0.5735764363510431618 ) ) ;
#15218=ORIENTED_EDGE ( 'NONE', *, *, #10553, .F. ) ;
#15268=CARTESIAN_POINT ( 'NONE',  ( -4.000000000000100364, 2.309401076758546445, -3.433295621305381573 ) ) ;
#15270=CARTESIAN_POINT ( 'NONE',  ( -3.680118525130293250, 2.494084732383297531, -0.3507732604232518536 ) ) ;
#15275=EDGE_CURVE ( 'NONE', #19106, #11464, #2779, .T. ) ;
#15290=PRODUCT_DEFINITION_SHAPE ( 'NONE', 'NONE',  #4448 ) ;
#15326=CARTESIAN_POINT ( 'NONE',  ( 3.999999999999619860, -1.677850389431014166, -3.535268758348135698 ) ) ;
#15339=VERTEX_POINT ( 'NONE', #385 ) ;
#15363=CARTESIAN_POINT ( 'NONE',  ( -5.560781378645589967, 7.794222813499895943E-15, -4.000000000000000000 ) ) ;
#15393=ORIENTED_EDGE ( 'NONE', *, *, #17733, .F. ) ;
#15398=ORIENTED_EDGE ( 'NONE', *, *, #1360, .T. ) ;
#15408=CARTESIAN_POINT ( 'NONE',  ( 2.344047193898538772, 3.265465875126504880, -2.077348303141170793E-15 ) ) ;
#15413=CARTESIAN_POINT ( 'NONE',  ( 0.000000000000000000, 0.000000000000000000, 0.000000000000000000 ) ) ;
#15440=CARTESIAN_POINT ( 'NONE',  ( 0.6920835326022192202, 4.454600218803903111, -3.597382984111570092 ) ) ;
#15490=CARTESIAN_POINT ( 'NONE',  ( 3.999999999999955147, -2.309401076758532678, -3.433295621305388678 ) ) ;
#15497=CIRCLE ( 'NONE', #5743, 2.500000000000015543 ) ;
#15514=VERTEX_POINT ( 'NONE', #11528 ) ;
#15561=CARTESIAN_POINT ( 'NONE',  ( 0.000000000000000000, 0.000000000000000000, -4.484454397937119197 ) ) ;
#15567=CARTESIAN_POINT ( 'NONE',  ( -3.999999999999735323, 0.8576368993457454959, -3.433240632782417645 ) ) ;
#15580=EDGE_CURVE ( 'NONE', #6911, #20801, #16543, .T. ) ;
#15622=EDGE_CURVE ( 'NONE', #7652, #8024, #4932, .T. ) ;
#15644=DIRECTION ( 'NONE',  ( -1.000000000000000000, 1.276756478318923119E-15, -1.333893503340766797E-15 ) ) ;
#15657=CARTESIAN_POINT ( 'NONE',  ( 0.000000000000000000, 0.000000000000000000, 0.000000000000000000 ) ) ;
#15662=AXIS2_PLACEMENT_3D ( 'NONE', #6782, #23146, #19597 ) ;
#15689=CARTESIAN_POINT ( 'NONE',  ( -4.000000000000058620, -2.309401076758546445, -3.433295621305388678 ) ) ;
#15690=ORIENTED_EDGE ( 'NONE', *, *, #21187, .T. ) ;
#15737=CARTESIAN_POINT ( 'NONE',  ( -0.5276280594138318403, 4.314175951382505758, -3.320322319201708616 ) ) ;
#15749=CARTESIAN_POINT ( 'NONE',  ( -0.1750025118122067458, -4.719839900820679723, -3.469254087858268054 ) ) ;
#15765=PRODUCT_DEFINITION_FORMATION_WITH_SPECIFIED_SOURCE ( 'ANY', '', #2909, .NOT_KNOWN. ) ;
#15771=ORIENTED_EDGE ( 'NONE', *, *, #15275, .T. ) ;
#15772=VERTEX_POINT ( 'NONE', #10373 ) ;
#15773=DIRECTION ( 'NONE',  ( -1.000000000000000000, 1.276756478318923119E-15, -1.239088197126283964E-15 ) ) ;
#15788=CARTESIAN_POINT ( 'NONE',  ( -4.197312064133520870, -0.8182229787991075476, -3.502518405183900008 ) ) ;
#15854=CARTESIAN_POINT ( 'NONE',  ( 0.6640947660599267888, -4.471078309994690692, -3.602146406945891943 ) ) ;
#15865=CARTESIAN_POINT ( 'NONE',  ( 1.999999999999953149, -3.464101615137771262, 0.000000000000000000 ) ) ;
#15881=VERTEX_POINT ( 'NONE', #22449 ) ;
#15883=ORIENTED_EDGE ( 'NONE', *, *, #14407, .T. ) ;
#15885=CARTESIAN_POINT ( 'NONE',  ( -4.211140560182305315, -2.431303136016589761, -3.745885042887437510 ) ) ;
#15899=DIRECTION ( 'NONE',  ( 1.333893503340774882E-15, 2.778352770573747380E-17, 1.000000000000000000 ) ) ;
#15974=CARTESIAN_POINT ( 'NONE',  ( 4.141042297810574091, -2.227970268150456068, -3.687027686973618934 ) ) ;
#15981=CARTESIAN_POINT ( 'NONE',  ( -2.000000000000036415, 3.464101615137757495, 0.000000000000000000 ) ) ;
#15982=CARTESIAN_POINT ( 'NONE',  ( 0.000000000000000000, 0.000000000000000000, -5.000000000000000888 ) ) ;
#15988=CARTESIAN_POINT ( 'NONE',  ( -4.000000000000098588, -0.7890432684750791070, -0.04868663549888898462 ) ) ;
#16007=DIRECTION ( 'NONE',  ( -1.333893503340774882E-15, -2.778352770573747380E-17, -1.000000000000000000 ) ) ;
#16033=ORIENTED_EDGE ( 'NONE', *, *, #17733, .T. ) ;
#16102=PRESENTATION_STYLE_ASSIGNMENT (( #9182 ) ) ;
#16105=CARTESIAN_POINT ( 'NONE',  ( 3.999999999999939160, 0.3987449864459891025, -0.01220643443054973340 ) ) ;
#16159=CARTESIAN_POINT ( 'NONE',  ( -3.540020015735878545, -2.810662092924825384, -3.602146406946029611 ) ) ;
#16167=( LENGTH_UNIT ( ) NAMED_UNIT ( * ) SI_UNIT ( .MILLI., .METRE. ) );
#16193=FACE_OUTER_BOUND ( 'NONE', #1913, .T. ) ;
#16201=CARTESIAN_POINT ( 'NONE',  ( -0.02448733951244273441, -4.877042772274788440, -3.751161874094042226 ) ) ;
#16214=CARTESIAN_POINT ( 'NONE',  ( -4.000000000000099476, -1.942223658245629148, -0.3516579909968203799 ) ) ;
#16264=DIRECTION ( 'NONE',  ( 0.5000000000000012212, -0.8660254037844379305, 6.428855108704667908E-16 ) ) ;
#16265=CIRCLE ( 'NONE', #15146, 2.500000000000015543 ) ;
#16273=DIRECTION ( 'NONE',  ( -1.000000000000000000, 1.276756478318922922E-15, -1.333893503340766797E-15 ) ) ;
#16278=CARTESIAN_POINT ( 'NONE',  ( -3.453038570459517675, -2.625189405340010218, -3.535263753544271470 ) ) ;
#16339=CARTESIAN_POINT ( 'NONE',  ( 3.999999999999955147, -2.309401076758532678, -3.433295621305388678 ) ) ;
#16343=( LENGTH_UNIT ( ) NAMED_UNIT ( * ) SI_UNIT ( .MILLI., .METRE. ) );
#16379=PLANE ( 'NONE',  #13258 ) ;
#16396=DIRECTION ( 'NONE',  ( -1.000000000000000000, 1.276756478318922725E-15, -1.333893503340766402E-15 ) ) ;
#16403=EDGE_CURVE ( 'NONE', #22731, #14190, #361, .T. ) ;
#16420=DIRECTION ( 'NONE',  ( 1.333893503340774882E-15, 2.778352770573747380E-17, 1.000000000000000000 ) ) ;
#16453=CARTESIAN_POINT ( 'NONE',  ( 1.144235203016624736, 3.958177651039125777, -0.09382832055447234976 ) ) ;
#16498=CARTESIAN_POINT ( 'NONE',  ( 4.197393957002242715, -0.4069871074557576685, -3.503767560748912491 ) ) ;
#16502=ADVANCED_FACE ( 'NONE', ( #11827 ), #20787, .F. ) ;
#16507=LINE ( 'NONE', #11106, #9675 ) ;
#16523=CARTESIAN_POINT ( 'NONE',  ( -2.000000000000119904, -3.464101615137792134, -1.040834085586084257E-14 ) ) ;
#16529=DIRECTION ( 'NONE',  ( 1.000000000000000000, -1.276756478318922922E-15, 1.288690253661653294E-15 ) ) ;
#16531=ADVANCED_FACE ( 'NONE', ( #3809, #72 ), #19819, .F. ) ;
#16533=B_SPLINE_CURVE_WITH_KNOTS ( 'NONE', 3,
 ( #2864, #15440, #10502, #14151, #1685, #21458, #21342, #1793 ),
 .UNSPECIFIED., .F., .F.,
 ( 4, 2, 2, 4 ),
 ( 0.000000000000000000, 0.002450665683189821864, 0.003675998524784732796, 0.004901331366379644595 ),
 .UNSPECIFIED. ) ;
#16543=LINE ( 'NONE', #9395, #22227 ) ;
#16564=ORIENTED_EDGE ( 'NONE', *, *, #6913, .F. ) ;
#16583=CARTESIAN_POINT ( 'NONE',  ( -4.000000000000107470, 2.309401076758546445, -0.4999999999999865663 ) ) ;
#16599=ORIENTED_EDGE ( 'NONE', *, *, #8798, .T. ) ;
#16610=CIRCLE ( 'NONE', #12488, 2.100000000000011635 ) ;
#16627=FACE_OUTER_BOUND ( 'NONE', #13898, .T. ) ;
#16652=CARTESIAN_POINT ( 'NONE',  ( -6.938893903907228378E-14, -4.618802153517121312, -5.000000000000011546 ) ) ;
#16688=ORIENTED_EDGE ( 'NONE', *, *, #10553, .T. ) ;
#16721=ORIENTED_EDGE ( 'NONE', *, *, #4653, .F. ) ;
#16723=ORIENTED_EDGE ( 'NONE', *, *, #3761, .F. ) ;
#16808=DIRECTION ( 'NONE',  ( 1.000000000000000000, -1.276756478318923119E-15, 1.387778780781436998E-15 ) ) ;
#16853=CARTESIAN_POINT ( 'NONE',  ( -4.000000000000103917, 2.309401076758544225, -3.504269196027523403 ) ) ;
#16860=CARTESIAN_POINT ( 'NONE',  ( 5.384454397937147974, -6.874637034779069804E-15, -4.999999999999993783 ) ) ;
#16861=CARTESIAN_POINT ( 'NONE',  ( 0.000000000000000000, 0.000000000000000000, 3.469446951953614189E-15 ) ) ;
#16886=DIRECTION ( 'NONE',  ( -1.000000000000000000, 1.276756478318923119E-15, -1.333893503340766797E-15 ) ) ;
#16918=VERTEX_POINT ( 'NONE', #5559 ) ;
#16923=CARTESIAN_POINT ( 'NONE',  ( 3.333333333333280191, -2.694301256218290419, -3.300726591567090473 ) ) ;
#17001=EDGE_CURVE ( 'NONE', #19280, #11464, #2366, .T. ) ;
#17005=ORIENTED_EDGE ( 'NONE', *, *, #18013, .F. ) ;
#17008=ORIENTED_EDGE ( 'NONE', *, *, #9500, .F. ) ;
#17063=AXIS2_PLACEMENT_3D ( 'NONE', #17286, #22596, #13542 ) ;
#17113=CARTESIAN_POINT ( 'NONE',  ( -4.000000000000045297, 1.387778780781445676E-14, 0.000000000000000000 ) ) ;
#17132=CARTESIAN_POINT ( 'NONE',  ( 0.000000000000000000, 0.000000000000000000, -5.000000000000000888 ) ) ;
#17151=ORIENTED_EDGE ( 'NONE', *, *, #3735, .F. ) ;
#17156=AXIS2_PLACEMENT_3D ( 'NONE', #16861, #20766, #22522 ) ;
#17202=CARTESIAN_POINT ( 'NONE',  ( 3.999999999999980016, 1.680228229147109786, -3.316631783032607750 ) ) ;
#17267=CARTESIAN_POINT ( 'NONE',  ( -4.000000000000107470, 2.309401076758546445, -0.4999999999999865663 ) ) ;
#17275=VERTEX_POINT ( 'NONE', #7305 ) ;
#17280=EDGE_CURVE ( 'NONE', #15772, #22002, #18555, .T. ) ;
#17286=CARTESIAN_POINT ( 'NONE',  ( 0.000000000000000000, 0.000000000000000000, 0.000000000000000000 ) ) ;
#17323=FACE_OUTER_BOUND ( 'NONE', #6976, .T. ) ;
#17330=ORIENTED_EDGE ( 'NONE', *, *, #7212, .T. ) ;
#17333=ORIENTED_EDGE ( 'NONE', *, *, #19879, .F. ) ;
#17339=DIRECTION ( 'NONE',  ( -1.000000000000000000, 1.276756478318922725E-15, -1.333893503340766402E-15 ) ) ;
#17431=B_SPLINE_CURVE_WITH_KNOTS ( 'NONE', 3,
 ( #3299, #12212, #18103, #10468, #14464, #23183, #19522, #6947 ),
 .UNSPECIFIED., .F., .F.,
 ( 4, 2, 2, 4 ),
 ( 2.465131516947375851E-07, 0.001183067374689833733, 0.001774477805458903349, 0.002365888236227973399 ),
 .UNSPECIFIED. ) ;
#17442=AXIS2_PLACEMENT_3D ( 'NONE', #19793, #3674, #17914 ) ;
#17443=CLOSED_SHELL ( 'NONE', ( #9728, #13298, #18599, #894, #7365, #3369, #4156, #13119, #4053, #785, #8375, #8258, #21890, #16531, #4109, #4236, #5051, #13419, #855, #13765, #4059, #5674, #7875, #17702, #9217, #22912, #11517, #21307, #8846, #11653, #19304, #16502 ) ) ;
#17455=EDGE_LOOP ( 'NONE', ( #20510, #15398, #16599, #5575, #7688, #14856, #14998 ) ) ;
#17509=ORIENTED_EDGE ( 'NONE', *, *, #23005, .F. ) ;
#17562=AXIS2_PLACEMENT_3D ( 'NONE', #767, #14524, #415 ) ;
#17591=DIRECTION ( 'NONE',  ( -1.333893503340774882E-15, -2.778352770573747380E-17, -1.000000000000000000 ) ) ;
#17647=( NAMED_UNIT ( * ) SI_UNIT ( $, .STERADIAN. ) SOLID_ANGLE_UNIT ( ) );
#17678=EDGE_CURVE ( 'NONE', #22641, #15514, #3638, .T. ) ;
#17702=ADVANCED_FACE ( 'NONE', ( #21374 ), #9262, .F. ) ;
#17716=AXIS2_PLACEMENT_3D ( 'NONE', #12798, #2214, #11371 ) ;
#17733=EDGE_CURVE ( 'NONE', #15514, #6911, #6188, .T. ) ;
#17768=CARTESIAN_POINT ( 'NONE',  ( 3.999999999999960032, -2.309401076758530902, -3.504271511726785082 ) ) ;
#17770=CARTESIAN_POINT ( 'NONE',  ( 3.999999999999948042, 2.309401076758532678, -5.000000000000000888 ) ) ;
#17783=APPLICATION_CONTEXT ( 'automotive_design' ) ;
#17808=CARTESIAN_POINT ( 'NONE',  ( -4.000000000000476952, -0.8232339106132060547, -3.430630286862590417 ) ) ;
#17810=ORIENTED_EDGE ( 'NONE', *, *, #7212, .F. ) ;
#17814=B_SPLINE_CURVE_WITH_KNOTS ( 'NONE', 3,
 ( #15689, #5594, #7577, #20166, #18282 ),
 .UNSPECIFIED., .F., .F.,
 ( 4, 1, 4 ),
 ( 0.000000000000000000, 0.002309401076758508826, 0.004618802153517017652 ),
 .UNSPECIFIED. ) ;
#17833=CARTESIAN_POINT ( 'NONE',  ( -4.204015924366279577, 1.626724848190933770, -3.610627190413417509 ) ) ;
#17837=CARTESIAN_POINT ( 'NONE',  ( 0.000000000000000000, 0.000000000000000000, -4.974599999999998801 ) ) ;
#17840=( NAMED_UNIT ( * ) SI_UNIT ( $, .STERADIAN. ) SOLID_ANGLE_UNIT ( ) );
#17893=EDGE_CURVE ( 'NONE', #2089, #15881, #5052, .T. ) ;
#17906=CARTESIAN_POINT ( 'NONE',  ( 0.000000000000000000, 0.000000000000000000, -4.000000000000000000 ) ) ;
#17914=DIRECTION ( 'NONE',  ( 1.000000000000000000, -1.276756478318922922E-15, 1.288690253661653294E-15 ) ) ;
#17923=CARTESIAN_POINT ( 'NONE',  ( -4.000000000000107470, -1.680117682357857412, -3.316611593219131571 ) ) ;
#17945=CARTESIAN_POINT ( 'NONE',  ( -4.198928548860862087, 0.8158838809860016195, -3.526471437616944815 ) ) ;
#17951=( BOUNDED_SURFACE ( )  B_SPLINE_SURFACE ( 3, 2, ( 
 ( #15749, #8584, #16201 ),
 ( #10806, #3412, #15854 ),
 ( #1643, #5053, #17999 ),
 ( #14231, #116, #21421 ),
 ( #14463, #10573, #21647 ),
 ( #8822, #15974, #1408 ) ),
 .UNSPECIFIED., .F., .F., .T. ) 
 B_SPLINE_SURFACE_WITH_KNOTS ( ( 4, 2, 4 ),
 ( 3, 3 ),
 ( 0.02032853247518128306, 0.02278863295364823988, 0.02524873343211519669 ),
 ( 0.000000000000000000, 1.000000000000000000 ),
 .UNSPECIFIED. ) 
 GEOMETRIC_REPRESENTATION_ITEM ( )  RATIONAL_B_SPLINE_SURFACE ( (
 ( 1.000000000000000000, 0.8047781615896822949, 1.000000000000000000),
 ( 1.000000000000000000, 0.8123767586288903608, 1.000000000000000000),
 ( 1.000000000000000000, 0.8190662415564858856, 1.000000000000000000),
 ( 1.000000000000000000, 0.8192361015668548907, 1.000000000000000000),
 ( 1.000000000000000000, 0.8126135807104273301, 1.000000000000000000),
 ( 1.000000000000000000, 0.8047712338318591119, 1.000000000000000000) ) ) 
 REPRESENTATION_ITEM ( '' )  SURFACE ( )  );
#17999=CARTESIAN_POINT ( 'NONE',  ( 1.360585162434879036, -4.061296242128364042, -3.505054077164883264 ) ) ;
#18007=( GEOMETRIC_REPRESENTATION_CONTEXT ( 3 ) GLOBAL_UNCERTAINTY_ASSIGNED_CONTEXT ( ( #4839 ) ) GLOBAL_UNIT_ASSIGNED_CONTEXT ( ( #16167, #85, #17840 ) ) REPRESENTATION_CONTEXT ( 'NONE', 'WORKASPACE' ) );
#18009=CARTESIAN_POINT ( 'NONE',  ( 3.999999999999952482, -1.539600717839022082, -3.300726591567082036 ) ) ;
#18013=EDGE_CURVE ( 'NONE', #6303, #7694, #16533, .T. ) ;
#18027=CARTESIAN_POINT ( 'NONE',  ( 0.000000000000000000, 0.000000000000000000, -4.694516984716116781 ) ) ;
#18051=EDGE_LOOP ( 'NONE', ( #7592, #10741, #17330, #21473, #1248 ) ) ;
#18052=EDGE_CURVE ( 'NONE', #9560, #15339, #18146, .T. ) ;
#18057=DIRECTION ( 'NONE',  ( 0.8660254037844379305, 0.5000000000000012212, 1.169077423688995342E-15 ) ) ;
#18066=CARTESIAN_POINT ( 'NONE',  ( -2.742827927723580306, -3.035229711104924899, -3.433252694550618767 ) ) ;
#18103=CARTESIAN_POINT ( 'NONE',  ( 3.355112389629148151, -2.681727112203222241, -0.2256878752776871611 ) ) ;
#18119=CARTESIAN_POINT ( 'NONE',  ( 3.999999999999955147, -3.469446951953614189E-14, 0.000000000000000000 ) ) ;
#18146=LINE ( 'NONE', #3781, #4274 ) ;
#18166=ORIENTED_EDGE ( 'NONE', *, *, #2185, .T. ) ;
#18177=EDGE_CURVE ( 'NONE', #7694, #10905, #21612, .T. ) ;
#18231=CARTESIAN_POINT ( 'NONE',  ( -4.024497503033626522, -2.323544716729399884, -3.572167766733401528 ) ) ;
#18234=DIRECTION ( 'NONE',  ( -1.333893503340774882E-15, -2.778352770573747380E-17, -1.000000000000000000 ) ) ;
#18262=CONICAL_SURFACE ( 'NONE', #11496, 4.000000000000022204, 0.8911886515913840512 ) ;
#18264=CARTESIAN_POINT ( 'NONE',  ( 3.999999999999937828, -1.560351142792990142, -0.2242961665059441667 ) ) ;
#18282=CARTESIAN_POINT ( 'NONE',  ( -6.938893903907228378E-14, -4.618802153517121312, -3.433295621305409107 ) ) ;
#18290=DIRECTION ( 'NONE',  ( 1.333893503340774882E-15, 2.778352770573747380E-17, 1.000000000000000000 ) ) ;
#18334=ORIENTED_EDGE ( 'NONE', *, *, #18462, .F. ) ;
#18337=CARTESIAN_POINT ( 'NONE',  ( 0.000000000000000000, 0.000000000000000000, 3.469446951953614189E-15 ) ) ;
#18350=DIRECTION ( 'NONE',  ( 1.000000000000000000, -1.276756478318922922E-15, 1.342094922251465017E-15 ) ) ;
#18431=LINE ( 'NONE', #16652, #22883 ) ;
#18462=EDGE_CURVE ( 'NONE', #9560, #22731, #12288, .T. ) ;
#18468=ORIENTED_EDGE ( 'NONE', *, *, #20616, .T. ) ;
#18489=CARTESIAN_POINT ( 'NONE',  ( 3.999999999999955147, -2.309401076758532678, -0.5000000000000004441 ) ) ;
#18528=CONICAL_SURFACE ( 'NONE', #21552, 2.060000000000013820, 0.9599310885968820317 ) ;
#18530=ORIENTED_EDGE ( 'NONE', *, *, #17001, .T. ) ;
#18536=FACE_OUTER_BOUND ( 'NONE', #11587, .T. ) ;
#18554=VERTEX_POINT ( 'NONE', #10705 ) ;
#18555=B_SPLINE_CURVE_WITH_KNOTS ( 'NONE', 3,
 ( #15865, #21543, #7075, #19647, #3309, #5064 ),
 .UNSPECIFIED., .F., .F.,
 ( 4, 2, 4 ),
 ( 0.002365888236227973399, 0.003551327329835062430, 0.004736766423442151895 ),
 .UNSPECIFIED. ) ;
#18597=CARTESIAN_POINT ( 'NONE',  ( 0.6666666666666055674, -4.233901974057364015, -3.300726591567105572 ) ) ;
#18599=ADVANCED_FACE ( 'NONE', ( #709 ), #23054, .F. ) ;
#18616=ORIENTED_EDGE ( 'NONE', *, *, #10131, .T. ) ;
#18637=DIRECTION ( 'NONE',  ( 1.333893503340774882E-15, 2.778352770573747380E-17, 1.000000000000000000 ) ) ;
#18689=CARTESIAN_POINT ( 'NONE',  ( 1.312671235360332256, 3.860931062424256321, -0.05923475698271866291 ) ) ;
#18694=ORIENTED_EDGE ( 'NONE', *, *, #3735, .T. ) ;
#18707=DIRECTION ( 'NONE',  ( -0.8660254037844378194, -0.5000000000000014433, -1.169077423688995342E-15 ) ) ;
#18725=ORIENTED_EDGE ( 'NONE', *, *, #7234, .F. ) ;
#18730=ORIENTED_EDGE ( 'NONE', *, *, #6708, .T. ) ;
#18772=ORIENTED_EDGE ( 'NONE', *, *, #11815, .F. ) ;
#18868=CARTESIAN_POINT ( 'NONE',  ( 2.060000000000013820, -2.630118345336998747E-15, -0.3080913168122645374 ) ) ;
#18873=ORIENTED_EDGE ( 'NONE', *, *, #3128, .F. ) ;
#18876=( BOUNDED_SURFACE ( )  B_SPLINE_SURFACE ( 3, 2, ( 
 ( #8809, #1515, #3628 ),
 ( #15737, #22934, #23169 ),
 ( #6932, #14097, #21521 ),
 ( #106, #7051, #5158 ),
 ( #14221, #8688, #7284 ),
 ( #14326, #1850, #23268 ) ),
 .UNSPECIFIED., .F., .F., .T. ) 
 B_SPLINE_SURFACE_WITH_KNOTS ( ( 4, 2, 4 ),
 ( 3, 3 ),
 ( 0.02032853247518125878, 0.02278863295364821559, 0.02524873343211517240 ),
 ( 0.000000000000000000, 1.000000000000000000 ),
 .UNSPECIFIED. ) 
 GEOMETRIC_REPRESENTATION_ITEM ( )  RATIONAL_B_SPLINE_SURFACE ( (
 ( 1.000000000000000000, 0.8047781615896834051, 1.000000000000000000),
 ( 1.000000000000000000, 0.8123767586290329135, 1.000000000000000000),
 ( 1.000000000000000000, 0.8190662415562958154, 1.000000000000000000),
 ( 1.000000000000000000, 0.8192361015670447388, 1.000000000000000000),
 ( 1.000000000000000000, 0.8126135807102816688, 1.000000000000000000),
 ( 1.000000000000000000, 0.8047712338318578906, 1.000000000000000000) ) ) 
 REPRESENTATION_ITEM ( '' )  SURFACE ( )  );
#18937=CARTESIAN_POINT ( 'NONE',  ( -2.171643655288394648, 3.365003104552311441, 2.155275334288567213E-15 ) ) ;
#18956=CARTESIAN_POINT ( 'NONE',  ( -1.040834085586084257E-13, 4.862606272033151100, -3.745885042887441063 ) ) ;
#18971=UNCERTAINTY_MEASURE_WITH_UNIT (LENGTH_MEASURE( 1.000000000000000082E-05 ), #16343, 'distance_accuracy_value', 'NONE');
#18972=ORIENTED_EDGE ( 'NONE', *, *, #9821, .F. ) ;
#18985=CARTESIAN_POINT ( 'NONE',  ( 4.204115023516959759, -1.660442669500223012, -3.602151381774619132 ) ) ;
#19012=CARTESIAN_POINT ( 'NONE',  ( 0.000000000000000000, 1.387778780781445676E-14, -25.03750572909315508 ) ) ;
#19018=CARTESIAN_POINT ( 'NONE',  ( -4.000000000000095923, 0.1981133338132648469, -6.980680862638442631E-14 ) ) ;
#19053=ORIENTED_EDGE ( 'NONE', *, *, #16403, .T. ) ;
#19070=DIRECTION ( 'NONE',  ( -1.333893503340774882E-15, -2.778352770573747380E-17, -1.000000000000000000 ) ) ;
#19093=CARTESIAN_POINT ( 'NONE',  ( 4.000000000000349054, 0.8228435280415953290, -3.430609588141484423 ) ) ;
#19106=VERTEX_POINT ( 'NONE', #2310 ) ;
#19169=EDGE_LOOP ( 'NONE', ( #12499, #17005, #20069, #14047 ) ) ;
#19180=CARTESIAN_POINT ( 'NONE',  ( -6.778475372771961472E-14, -4.736529461165952526, -3.681130640444301605 ) ) ;
#19200=CARTESIAN_POINT ( 'NONE',  ( -4.197393957002396370, -0.8151795401431403132, -3.503767560748964449 ) ) ;
#19207=EDGE_CURVE ( 'NONE', #2089, #7096, #21195, .T. ) ;
#19210=FACE_OUTER_BOUND ( 'NONE', #5436, .T. ) ;
#19214=CARTESIAN_POINT ( 'NONE',  ( -3.999999999998684164, 1.677772373332598210, -3.535253723897363365 ) ) ;
#19237=CARTESIAN_POINT ( 'NONE',  ( 2.500000000000025313, -2.885729496010498622E-15, -4.974600000000002353 ) ) ;
#19267=B_SPLINE_CURVE_WITH_KNOTS ( 'NONE', 3,
 ( #17113, #19018, #8195, #914, #675, #3014, #6080, #22318 ),
 .UNSPECIFIED., .F., .F.,
 ( 4, 2, 2, 4 ),
 ( 0.005725059856848725010, 0.006314084072593702072, 0.006903108288338679135, 0.008081156719828633261 ),
 .UNSPECIFIED. ) ;
#19271=ORIENTED_EDGE ( 'NONE', *, *, #17280, .F. ) ;
#19280=VERTEX_POINT ( 'NONE', #19237 ) ;
#19304=ADVANCED_FACE ( 'NONE', ( #8656 ), #537, .F. ) ;
#19353=CARTESIAN_POINT ( 'NONE',  ( -0.6920835326022843903, -4.454600218803954625, -3.597382984111614945 ) ) ;
#19359=FACE_OUTER_BOUND ( 'NONE', #12471, .T. ) ;
#19411=( NAMED_UNIT ( * ) PLANE_ANGLE_UNIT ( ) SI_UNIT ( $, .RADIAN. ) );
#19417=AXIS2_PLACEMENT_3D ( 'NONE', #15413, #19070, #15644 ) ;
#19425=CARTESIAN_POINT ( 'NONE',  ( 1.274258131565143559, 3.883108878240837392, -3.220599429844244188 ) ) ;
#19445=CARTESIAN_POINT ( 'NONE',  ( -4.000000000000103029, 1.700094919196693644, -3.320312364301530206 ) ) ;
#19448=AXIS2_PLACEMENT_3D ( 'NONE', #11452, #14876, #5716 ) ;
#19455=ORIENTED_EDGE ( 'NONE', *, *, #11801, .T. ) ;
#19462=VECTOR ( 'NONE', #11977, 1000.000000000000000 ) ;
#19488=EDGE_LOOP ( 'NONE', ( #22389, #10714, #23142, #575 ) ) ;
#19509=FACE_OUTER_BOUND ( 'NONE', #6883, .T. ) ;
#19512=DIRECTION ( 'NONE',  ( 1.000000000000000000, -1.276756478318923119E-15, -1.333893503340774882E-15 ) ) ;
#19514=ORIENTED_EDGE ( 'NONE', *, *, #9500, .T. ) ;
#19522=CARTESIAN_POINT ( 'NONE',  ( 2.171643655288359565, -3.365003104552389157, -3.921216680110290851E-14 ) ) ;
#19536=CONICAL_SURFACE ( 'NONE', #4499, 4.000000000000022204, 0.8911886515913840512 ) ;
#19547=CARTESIAN_POINT ( 'NONE',  ( 2.756197834949904557, 3.027510591568840503, -3.223146290109631718 ) ) ;
#19563=CARTESIAN_POINT ( 'NONE',  ( -4.000000000000106581, -0.8382240730042997967, -3.220610619766981930 ) ) ;
#19574=EDGE_LOOP ( 'NONE', ( #15018, #22473, #18730, #23240 ) ) ;
#19596=SURFACE_STYLE_FILL_AREA ( #8660 ) ;
#19597=DIRECTION ( 'NONE',  ( 1.000000000000000000, -1.276756478318922725E-15, 1.333893503340766402E-15 ) ) ;
#19640=AXIS2_PLACEMENT_3D ( 'NONE', #6333, #806, #20919 ) ;
#19647=CARTESIAN_POINT ( 'NONE',  ( 0.6507732100473145875, -4.243078065514858999, -0.2236248678335386320 ) ) ;
#19666=ORIENTED_EDGE ( 'NONE', *, *, #17893, .F. ) ;
#19686=EDGE_CURVE ( 'NONE', #22849, #405, #12934, .T. ) ;
#19729=ORIENTED_EDGE ( 'NONE', *, *, #745, .T. ) ;
#19739=CARTESIAN_POINT ( 'NONE',  ( 4.197393957002244491, 7.205051708611501750E-14, -3.503767560748914711 ) ) ;
#19752=CARTESIAN_POINT ( 'NONE',  ( 3.999999999999955147, -3.469446951953614189E-14, 0.000000000000000000 ) ) ;
#19758=DIRECTION ( 'NONE',  ( -1.000000000000000000, 1.276756478318922922E-15, 1.333893503340774882E-15 ) ) ;
#19776=CARTESIAN_POINT ( 'NONE',  ( 3.999999999999938716, 0.7924765000094652345, -0.05906175389885159194 ) ) ;
#19785=CARTESIAN_POINT ( 'NONE',  ( 0.5636800770122561977, 4.293361309316750862, -3.531542292954451767 ) ) ;
#19793=CARTESIAN_POINT ( 'NONE',  ( 0.000000000000000000, 0.000000000000000000, -5.000000000000000888 ) ) ;
#19819=PLANE ( 'NONE',  #13629 ) ;
#19823=CARTESIAN_POINT ( 'NONE',  ( -1.390230914382294847, -4.043987460488769337, -3.502507215260536988 ) ) ;
#19832=SURFACE_STYLE_USAGE ( .BOTH. , #12413 ) ;
#19879=EDGE_CURVE ( 'NONE', #10484, #16918, #942, .T. ) ;
#19903=EDGE_CURVE ( 'NONE', #16918, #13467, #13112, .T. ) ;
#19904=CARTESIAN_POINT ( 'NONE',  ( 3.453038570459371570, 2.625189405339196647, -3.535263753544082288 ) ) ;
#19913=DIRECTION ( 'NONE',  ( 1.333893503340774882E-15, 2.778352770573747380E-17, 1.000000000000000000 ) ) ;
#19929=ORIENTED_EDGE ( 'NONE', *, *, #12539, .F. ) ;
#19933=EDGE_CURVE ( 'NONE', #2382, #14190, #20991, .T. ) ;
#19945=CARTESIAN_POINT ( 'NONE',  ( -0.5449313310647870834, -4.304185902836999311, -3.316620875263376789 ) ) ;
#19947=FACE_OUTER_BOUND ( 'NONE', #22770, .T. ) ;
#19960=DIRECTION ( 'NONE',  ( -1.000000000000000000, 1.276756478318923119E-15, -1.239088197126283964E-15 ) ) ;
#19998=CARTESIAN_POINT ( 'NONE',  ( 3.999999999999940936, 2.309401076758546445, -0.5000000000000004441 ) ) ;
#20028=CIRCLE ( 'NONE', #11382, 2.100000000000011635 ) ;
#20058=CARTESIAN_POINT ( 'NONE',  ( -2.500000000000002220, 1.793290614977871628E-14, -4.999999999999997335 ) ) ;
#20059=CARTESIAN_POINT ( 'NONE',  ( -4.211140560182312420, 2.431303136016568889, -3.745885042887433958 ) ) ;
#20069=ORIENTED_EDGE ( 'NONE', *, *, #13413, .T. ) ;
#20105=CARTESIAN_POINT ( 'NONE',  ( 6.844222713676473743E-15, 4.618802153517023612, -3.504269196027541167 ) ) ;
#20118=B_SPLINE_CURVE_WITH_KNOTS ( 'NONE', 3,
 ( #17267, #15270, #13640, #10333, #6809, #9878, #18937, #20937 ),
 .UNSPECIFIED., .F., .F.,
 ( 4, 2, 2, 4 ),
 ( 2.465131516885230102E-07, 0.001183067374689851514, 0.001774477805458931972, 0.002365888236228012864 ),
 .UNSPECIFIED. ) ;
#20141=CARTESIAN_POINT ( 'NONE',  ( 2.500000000000015543, -2.885729496010487183E-15, -4.974599999999995248 ) ) ;
#20166=CARTESIAN_POINT ( 'NONE',  ( -0.6666666666667374619, -4.233901974057366679, -3.300726591567110013 ) ) ;
#20170=EDGE_CURVE ( 'NONE', #6591, #18554, #2046, .T. ) ;
#20176=FACE_BOUND ( 'NONE', #23065, .T. ) ;
#20209=CARTESIAN_POINT ( 'NONE',  ( 0.000000000000000000, 0.000000000000000000, -5.000000000000000888 ) ) ;
#20227=FACE_OUTER_BOUND ( 'NONE', #13673, .T. ) ;
#20251=MECHANICAL_DESIGN_GEOMETRIC_PRESENTATION_REPRESENTATION('',(#22873),#18007);
#20358=CARTESIAN_POINT ( 'NONE',  ( 6.938893903907228378E-15, 4.618802153517023612, -5.000000000000000888 ) ) ;
#20381=EDGE_LOOP ( 'NONE', ( #6500, #3087, #14313, #624, #21062 ) ) ;
#20410=CARTESIAN_POINT ( 'NONE',  ( -2.060000000000013820, 2.882395585961355661E-15, -0.3080913168122700885 ) ) ;
#20415=ORIENTED_EDGE ( 'NONE', *, *, #19903, .F. ) ;
#20508=ORIENTED_EDGE ( 'NONE', *, *, #14327, .T. ) ;
#20510=ORIENTED_EDGE ( 'NONE', *, *, #18177, .T. ) ;
#20571=DIRECTION ( 'NONE',  ( 1.333893503340774882E-15, 2.778352770573747380E-17, 1.000000000000000000 ) ) ;
#20607=CARTESIAN_POINT ( 'NONE',  ( -6.938893903907228378E-14, -4.618802153517121312, -3.433295621305409107 ) ) ;
#20616=EDGE_CURVE ( 'NONE', #7096, #20801, #19267, .T. ) ;
#20622=ORIENTED_EDGE ( 'NONE', *, *, #11815, .T. ) ;
#20643=CARTESIAN_POINT ( 'NONE',  ( -4.000000000000100364, 2.309401076758546445, -3.433295621305381573 ) ) ;
#20677=DIRECTION ( 'NONE',  ( -1.333893503340774882E-15, -2.778352770573747380E-17, -1.000000000000000000 ) ) ;
#20766=DIRECTION ( 'NONE',  ( 1.333893503340774882E-15, 2.778352770573747380E-17, 1.000000000000000000 ) ) ;
#20768=EDGE_CURVE ( 'NONE', #13336, #19280, #388, .T. ) ;
#20787=CYLINDRICAL_SURFACE ( 'NONE', #15123, 2.500000000000015543 ) ;
#20801=VERTEX_POINT ( 'NONE', #16583 ) ;
#20837=VERTEX_POINT ( 'NONE', #13318 ) ;
#20919=DIRECTION ( 'NONE',  ( 0.8660254037844363761, -0.5000000000000037748, 1.141293895983254713E-15 ) ) ;
#20928=DIRECTION ( 'NONE',  ( 1.399221158233658267E-15, 1.000000000000000000, -2.778352770573934118E-17 ) ) ;
#20937=CARTESIAN_POINT ( 'NONE',  ( -2.000000000000036415, 3.464101615137757495, 0.000000000000000000 ) ) ;
#20945=EDGE_CURVE ( 'NONE', #7096, #10484, #1032, .T. ) ;
#20958=DIRECTION ( 'NONE',  ( -1.333893503340774882E-15, -2.778352770573747380E-17, -1.000000000000000000 ) ) ;
#20983=AXIS2_PLACEMENT_3D ( 'NONE', #8133, #20958, #1196 ) ;
#20991=B_SPLINE_CURVE_WITH_KNOTS ( 'NONE', 3,
 ( #20607, #13427, #4475, #19180, #3070, #2837 ),
 .UNSPECIFIED., .F., .F.,
 ( 4, 2, 4 ),
 ( 0.000000000000000000, 0.0002095117440854745035, 0.0004190234881709490071 ),
 .UNSPECIFIED. ) ;
#21055=MANIFOLD_SOLID_BREP ( 'EndChamfer', #17443 ) ;
#21062=ORIENTED_EDGE ( 'NONE', *, *, #3195, .F. ) ;
#21065=EDGE_CURVE ( 'NONE', #8464, #13467, #3314, .T. ) ;
#21075=EDGE_CURVE ( 'NONE', #17275, #16918, #12645, .T. ) ;
#21077=CARTESIAN_POINT ( 'NONE',  ( -4.000000000000100364, 2.309401076758546445, -3.433295621305381573 ) ) ;
#21186=DIRECTION ( 'NONE',  ( -1.000000000000000000, 1.276756478318923119E-15, -1.387778780781436998E-15 ) ) ;
#21187=EDGE_CURVE ( 'NONE', #9707, #6911, #6486, .T. ) ;
#21195=CIRCLE ( 'NONE', #904, 4.000000000000023093 ) ;
#21307=ADVANCED_FACE ( 'NONE', ( #19509 ), #18876, .F. ) ;
#21309=CARTESIAN_POINT ( 'NONE',  ( -4.000000000000098588, -1.560351142792954393, -0.2242961665060443921 ) ) ;
#21342=CARTESIAN_POINT ( 'NONE',  ( 3.861362476283208167, 2.629030857715989988, -3.671615880910374941 ) ) ;
#21374=FACE_OUTER_BOUND ( 'NONE', #4748, .T. ) ;
#21403=CARTESIAN_POINT ( 'NONE',  ( -6.938893903907228378E-14, -4.618802153517121312, -3.433295621305409107 ) ) ;
#21421=CARTESIAN_POINT ( 'NONE',  ( 2.807080416179122295, -3.225969019225178425, -3.502507215260535656 ) ) ;
#21458=CARTESIAN_POINT ( 'NONE',  ( 3.510273485745285083, 2.827716139362673076, -3.610536846335890449 ) ) ;
#21473=ORIENTED_EDGE ( 'NONE', *, *, #21075, .T. ) ;
#21481=DIRECTION ( 'NONE',  ( 1.333893503340766797E-15, -2.778352770574087576E-17, -1.000000000000000000 ) ) ;
#21485=AXIS2_PLACEMENT_3D ( 'NONE', #13393, #2569, #9866 ) ;
#21487=CARTESIAN_POINT ( 'NONE',  ( -4.101948962586009273, 2.368261337751074169, -3.681124513963648148 ) ) ;
#21494=( NAMED_UNIT ( * ) SI_UNIT ( $, .STERADIAN. ) SOLID_ANGLE_UNIT ( ) );
#21502=VECTOR ( 'NONE', #6769, 1000.000000000000114 ) ;
#21521=CARTESIAN_POINT ( 'NONE',  ( -1.360585162436302342, 4.061296242127595768, -3.505054077164885928 ) ) ;
#21538=ORIENTED_EDGE ( 'NONE', *, *, #8798, .F. ) ;
#21543=CARTESIAN_POINT ( 'NONE',  ( 1.655952806101401054, -3.662737355149109142, -4.567116948300461998E-14 ) ) ;
#21552=AXIS2_PLACEMENT_3D ( 'NONE', #13800, #12374, #4852 ) ;
#21560=CARTESIAN_POINT ( 'NONE',  ( 1.287237434361995003, 3.875615274277167455, -3.430618716627008791 ) ) ;
#21572=CARTESIAN_POINT ( 'NONE',  ( 5.384454397937147974, -6.874637034779069804E-15, -4.484454397937112979 ) ) ;
#21578=CARTESIAN_POINT ( 'NONE',  ( 3.999999999999955147, -3.469446951953614189E-14, 0.000000000000000000 ) ) ;
#21603=CARTESIAN_POINT ( 'NONE',  ( -0.6810597143203314108, -4.461075778260221725, -3.598441714920940449 ) ) ;
#21605=CARTESIAN_POINT ( 'NONE',  ( 3.999999999999948042, 2.309401076758532678, -5.000000000000000888 ) ) ;
#21612=B_SPLINE_CURVE_WITH_KNOTS ( 'NONE', 3,
 ( #2254, #4012, #9553, #5683 ),
 .UNSPECIFIED., .F., .F.,
 ( 4, 4 ),
 ( 0.000000000000000000, 0.002452478801916372839 ),
 .UNSPECIFIED. ) ;
#21622=DIRECTION ( 'NONE',  ( 1.333893503340774882E-15, 2.778352770573747380E-17, 1.000000000000000000 ) ) ;
#21647=CARTESIAN_POINT ( 'NONE',  ( 3.522875095018858094, -2.820352903224746743, -3.598441714920217471 ) ) ;
#21673=CARTESIAN_POINT ( 'NONE',  ( 3.540020015735602765, 2.810662092923783550, -3.602146406945765822 ) ) ;
#21689=B_SPLINE_CURVE_WITH_KNOTS ( 'NONE', 3,
 ( #1586, #19353, #3250, #8766, #10412, #7702, #7244, #9582 ),
 .UNSPECIFIED., .F., .F.,
 ( 4, 2, 2, 4 ),
 ( 0.000000000000000000, 0.002450665683189822731, 0.003675998524784734097, 0.004901331366379645463 ),
 .UNSPECIFIED. ) ;
#21712=CARTESIAN_POINT ( 'NONE',  ( -4.175002511812232697, -2.208363329454933410, -3.469254087858270719 ) ) ;
#21724=AXIS2_PLACEMENT_3D ( 'NONE', #15982, #3419, #12457 ) ;
#21734=CARTESIAN_POINT ( 'NONE',  ( -0.3198814748698700083, -4.434118497892228561, -0.3507732604232856044 ) ) ;
#21794=CARTESIAN_POINT ( 'NONE',  ( 0.000000000000000000, 0.000000000000000000, -4.974599999999998801 ) ) ;
#21828=EDGE_CURVE ( 'NONE', #6591, #20837, #11455, .T. ) ;
#21862=ORIENTED_EDGE ( 'NONE', *, *, #18052, .T. ) ;
#21869=CARTESIAN_POINT ( 'NONE',  ( 2.661839581153344325E-13, 4.796734841935159643, -3.721909803043225828 ) ) ;
#21890=ADVANCED_FACE ( 'NONE', ( #17323 ), #2871, .T. ) ;
#21892=EDGE_CURVE ( 'NONE', #7256, #20837, #8916, .T. ) ;
#21999=CARTESIAN_POINT ( 'NONE',  ( 0.6448876103707898988, 4.246476118072396666, -0.2256878752776944885 ) ) ;
#22002=VERTEX_POINT ( 'NONE', #5102 ) ;
#22009=FACE_OUTER_BOUND ( 'NONE', #177, .T. ) ;
#22045=CARTESIAN_POINT ( 'NONE',  ( 4.207491450040564018, -2.029819825146498502, -3.671670828759570959 ) ) ;
#22103=LINE ( 'NONE', #2099, #22295 ) ;
#22115=AXIS2_PLACEMENT_3D ( 'NONE', #4943, #2963, #5306 ) ;
#22124=CARTESIAN_POINT ( 'NONE',  ( 3.999999999999955147, -2.309401076758532678, -3.433295621305388678 ) ) ;
#22225=DIRECTION ( 'NONE',  ( 1.000000000000000000, -1.276756478318923119E-15, 1.239088197126283964E-15 ) ) ;
#22227=VECTOR ( 'NONE', #3738, 1000.000000000000000 ) ;
#22234=EDGE_LOOP ( 'NONE', ( #5517, #631, #15771, #13232 ) ) ;
#22272=CARTESIAN_POINT ( 'NONE',  ( 3.999999999999948042, 2.309401076758532678, -3.433295621305378020 ) ) ;
#22295=VECTOR ( 'NONE', #237, 1000.000000000000000 ) ;
#22298=VERTEX_POINT ( 'NONE', #19752 ) ;
#22299=AXIS2_PLACEMENT_3D ( 'NONE', #20358, #7888, #18707 ) ;
#22317=EDGE_CURVE ( 'NONE', #10484, #17275, #4730, .T. ) ;
#22318=CARTESIAN_POINT ( 'NONE',  ( -4.000000000000107470, 2.309401076758546445, -0.4999999999999865663 ) ) ;
#22349=FACE_OUTER_BOUND ( 'NONE', #1461, .T. ) ;
#22365=CARTESIAN_POINT ( 'NONE',  ( -5.384454397937119552, 7.656970828559639486E-15, -4.999999999999993783 ) ) ;
#22389=ORIENTED_EDGE ( 'NONE', *, *, #21828, .F. ) ;
#22401=DIRECTION ( 'NONE',  ( 1.000000000000000000, -1.276756478318923119E-15, -1.333893503340774882E-15 ) ) ;
#22410=CONICAL_SURFACE ( 'NONE', #11874, 5.560781378645605066, 1.221730476396047704 ) ;
#22449=CARTESIAN_POINT ( 'NONE',  ( -4.000000000000087041, -2.309401076758553550, -0.5000000000000004441 ) ) ;
#22454=CIRCLE ( 'NONE', #21724, 2.500000000000015543 ) ;
#22473=ORIENTED_EDGE ( 'NONE', *, *, #21828, .T. ) ;
#22484=CARTESIAN_POINT ( 'NONE',  ( -1.747541505913290161, 3.837784562140251765, -3.503702292528905193 ) ) ;
#22511=AXIS2_PLACEMENT_3D ( 'NONE', #2409, #14881, #16396 ) ;
#22522=DIRECTION ( 'NONE',  ( 1.000000000000000000, -1.276756478318922922E-15, 1.333893503340766994E-15 ) ) ;
#22592=LINE ( 'NONE', #11414, #14673 ) ;
#22596=DIRECTION ( 'NONE',  ( -1.333893503340774882E-15, -2.778352770573747380E-17, -1.000000000000000000 ) ) ;
#22629=CARTESIAN_POINT ( 'NONE',  ( -2.682243648011765735, -3.070208061305350622, -0.04852650426608514506 ) ) ;
#22641=VERTEX_POINT ( 'NONE', #8898 ) ;
#22655=ORIENTED_EDGE ( 'NONE', *, *, #11801, .F. ) ;
#22662=FACE_OUTER_BOUND ( 'NONE', #8298, .T. ) ;
#22669=EDGE_CURVE ( 'NONE', #22298, #16918, #13814, .T. ) ;
#22704=CARTESIAN_POINT ( 'NONE',  ( 6.938893903907228378E-15, 4.618802153517023612, -5.000000000000000888 ) ) ;
#22706=ORIENTED_EDGE ( 'NONE', *, *, #10990, .F. ) ;
#22715=DIRECTION ( 'NONE',  ( 1.333893503340774882E-15, 2.778352770573747380E-17, 1.000000000000000000 ) ) ;
#22731=VERTEX_POINT ( 'NONE', #5010 ) ;
#22760=ORIENTED_EDGE ( 'NONE', *, *, #14327, .F. ) ;
#22770=EDGE_LOOP ( 'NONE', ( #1492, #18972, #4492, #4702 ) ) ;
#22788=EDGE_LOOP ( 'NONE', ( #22760, #17008, #7967, #18530 ) ) ;
#22798=EDGE_CURVE ( 'NONE', #18554, #7256, #4627, .T. ) ;
#22814=CARTESIAN_POINT ( 'NONE',  ( -0.6666666666666698493, 4.233901974057265427, -3.300726591567082036 ) ) ;
#22815=LINE ( 'NONE', #22704, #19462 ) ;
#22817=ORIENTED_EDGE ( 'NONE', *, *, #174, .F. ) ;
#22828=CIRCLE ( 'NONE', #2926, 2.500000000000014655 ) ;
#22849=VERTEX_POINT ( 'NONE', #16860 ) ;
#22870=CARTESIAN_POINT ( 'NONE',  ( -4.197477534772400709, 0.8522413273724812610, -3.505042416683278983 ) ) ;
#22873=STYLED_ITEM ( 'NONE', ( #6780 ), #5834 ) ;
#22883=VECTOR ( 'NONE', #16420, 1000.000000000000000 ) ;
#22912=ADVANCED_FACE ( 'NONE', ( #6629 ), #13178, .F. ) ;
#22934=CARTESIAN_POINT ( 'NONE',  ( -0.5469614295398264048, 4.303013824934858178, -3.535263753543724352 ) ) ;
#22952=DIRECTION ( 'NONE',  ( -1.333893503340774882E-15, -2.778352770573747380E-17, -1.000000000000000000 ) ) ;
#23005=EDGE_CURVE ( 'NONE', #15339, #22298, #11184, .T. ) ;
#23044=CIRCLE ( 'NONE', #8395, 5.560781378645605066 ) ;
#23054=CONICAL_SURFACE ( 'NONE', #133, 2.060000000000013820, 0.9599310885968820317 ) ;
#23065=EDGE_LOOP ( 'NONE', ( #19514, #12946 ) ) ;
#23136=DIRECTION ( 'NONE',  ( -1.333893503340774882E-15, -2.778352770573747380E-17, -1.000000000000000000 ) ) ;
#23142=ORIENTED_EDGE ( 'NONE', *, *, #22798, .T. ) ;
#23146=DIRECTION ( 'NONE',  ( 1.333893503340774882E-15, 2.778352770573747380E-17, 1.000000000000000000 ) ) ;
#23149=EDGE_CURVE ( 'NONE', #6911, #11666, #13108, .T. ) ;
#23169=CARTESIAN_POINT ( 'NONE',  ( -0.6640947660583549350, 4.471078309994097388, -3.602146406945683221 ) ) ;
#23181=FACE_OUTER_BOUND ( 'NONE', #2033, .T. ) ;
#23183=CARTESIAN_POINT ( 'NONE',  ( 2.345747346278090451, -3.264484291692558937, -0.01223254789877006345 ) ) ;
#23192=CARTESIAN_POINT ( 'NONE',  ( 3.999999999999948042, 2.309401076758532678, -3.433295621305378020 ) ) ;
#23222=FACE_OUTER_BOUND ( 'NONE', #19488, .T. ) ;
#23240=ORIENTED_EDGE ( 'NONE', *, *, #22798, .F. ) ;
#23268=CARTESIAN_POINT ( 'NONE',  ( -4.236525694536651621, 2.416953475386471872, -3.751298745799860335 ) ) ;
ENDSEC;
END-ISO-10303-21;
